ISO-10303-21;
HEADER;
/* Generated by software containing ST-Developer
 * from STEP Tools, Inc. (www.steptools.com) 
 */

FILE_DESCRIPTION(
/* description */ (''),
/* implementation_level */ '2;1');

FILE_NAME(
/* name */ '02_Piston_Ring_Turbine_D19.step',
/* time_stamp */ '2026-10-25T01:10:36-07:00',
/* author */ (''),
/* organization */ (''),
/* preprocessor_version */ 'ST-DEVELOPER v20.2',
/* originating_system */ 'Autodesk Translation Framework v15.15.0.0',
/* authorisation */ '');

FILE_SCHEMA (('AUTOMOTIVE_DESIGN { 1 0 10303 214 3 1 1 }'));
ENDSEC;

DATA;
#10=MECHANICAL_DESIGN_GEOMETRIC_PRESENTATION_REPRESENTATION('',(#1296),#60365);
#68=SHAPE_REPRESENTATION_RELATIONSHIP('SRR','None',#60408,#78);
#78=ADVANCED_BREP_SHAPE_REPRESENTATION('',(#88),#60356);
#88=MANIFOLD_SOLID_BREP('Body1',#18298);
#123=B_SPLINE_SURFACE_WITH_KNOTS('',3,3,((#41716,#41717,#41718,#41719,#41720,
#41721,#41722,#41723,#41724,#41725,#41726,#41727,#41728,#41729,#41730,#41731,
#41732),(#41733,#41734,#41735,#41736,#41737,#41738,#41739,#41740,#41741,
#41742,#41743,#41744,#41745,#41746,#41747,#41748,#41749),(#41750,#41751,
#41752,#41753,#41754,#41755,#41756,#41757,#41758,#41759,#41760,#41761,#41762,
#41763,#41764,#41765,#41766),(#41767,#41768,#41769,#41770,#41771,#41772,
#41773,#41774,#41775,#41776,#41777,#41778,#41779,#41780,#41781,#41782,#41783)),
 .UNSPECIFIED.,.F.,.F.,.F.,(4,4),(4,1,1,1,1,1,1,1,1,1,1,1,1,1,4),(0.,1.),
(0.,0.0714285714285714,0.142857142857143,0.214285714285714,0.285714285714286,
0.357142857142857,0.428571428571429,0.476190476190476,0.571428571428571,
0.619047619047619,0.714285714285714,0.785714285714286,0.857142857142857,
0.928571428571429,1.),.UNSPECIFIED.);
#124=B_SPLINE_SURFACE_WITH_KNOTS('',3,3,((#42606,#42607,#42608,#42609,#42610,
#42611,#42612,#42613,#42614,#42615,#42616,#42617,#42618,#42619,#42620,#42621,
#42622),(#42623,#42624,#42625,#42626,#42627,#42628,#42629,#42630,#42631,
#42632,#42633,#42634,#42635,#42636,#42637,#42638,#42639),(#42640,#42641,
#42642,#42643,#42644,#42645,#42646,#42647,#42648,#42649,#42650,#42651,#42652,
#42653,#42654,#42655,#42656),(#42657,#42658,#42659,#42660,#42661,#42662,
#42663,#42664,#42665,#42666,#42667,#42668,#42669,#42670,#42671,#42672,#42673)),
 .UNSPECIFIED.,.F.,.F.,.F.,(4,4),(4,1,1,1,1,1,1,1,1,1,1,1,1,1,4),(0.,1.),
(-3.39227166254691E-15,0.071428563366594,0.142857126733191,0.214285690099789,
0.285714253466386,0.380952337955183,0.428571380199581,0.523809464688377,
0.571428506932776,0.642857070299373,0.71428563366597,0.785714197032568,
0.857142760399165,0.928571323765762,0.99999988713236),.UNSPECIFIED.);
#125=B_SPLINE_SURFACE_WITH_KNOTS('',3,3,((#42696,#42697,#42698,#42699,#42700,
#42701,#42702,#42703,#42704,#42705,#42706,#42707,#42708,#42709,#42710,#42711),
(#42712,#42713,#42714,#42715,#42716,#42717,#42718,#42719,#42720,#42721,
#42722,#42723,#42724,#42725,#42726,#42727),(#42728,#42729,#42730,#42731,
#42732,#42733,#42734,#42735,#42736,#42737,#42738,#42739,#42740,#42741,#42742,
#42743),(#42744,#42745,#42746,#42747,#42748,#42749,#42750,#42751,#42752,
#42753,#42754,#42755,#42756,#42757,#42758,#42759),(#42760,#42761,#42762,
#42763,#42764,#42765,#42766,#42767,#42768,#42769,#42770,#42771,#42772,#42773,
#42774,#42775),(#42776,#42777,#42778,#42779,#42780,#42781,#42782,#42783,
#42784,#42785,#42786,#42787,#42788,#42789,#42790,#42791),(#42792,#42793,
#42794,#42795,#42796,#42797,#42798,#42799,#42800,#42801,#42802,#42803,#42804,
#42805,#42806,#42807),(#42808,#42809,#42810,#42811,#42812,#42813,#42814,
#42815,#42816,#42817,#42818,#42819,#42820,#42821,#42822,#42823),(#42824,
#42825,#42826,#42827,#42828,#42829,#42830,#42831,#42832,#42833,#42834,#42835,
#42836,#42837,#42838,#42839)),.UNSPECIFIED.,.F.,.F.,.F.,(4,1,1,1,1,1,4),
(4,1,1,1,1,1,1,1,1,1,1,1,1,4),(0.,0.0357142857142857,0.0714285714285714,
0.107142857142857,0.142857142857143,0.285714285714286,1.),(-1.31922727866773E-7,
0.0444444444444444,0.114351851851852,0.184259259259259,0.254166666666666,
0.324074074074073,0.39398148148148,0.463888888888888,0.55324074074074,0.642592592592592,
0.731944444444444,0.821296296296296,0.910648148148148,1.),.UNSPECIFIED.);
#126=B_SPLINE_SURFACE_WITH_KNOTS('',3,3,((#43632,#43633,#43634,#43635,#43636,
#43637,#43638,#43639,#43640,#43641,#43642,#43643,#43644,#43645,#43646,#43647,
#43648),(#43649,#43650,#43651,#43652,#43653,#43654,#43655,#43656,#43657,
#43658,#43659,#43660,#43661,#43662,#43663,#43664,#43665),(#43666,#43667,
#43668,#43669,#43670,#43671,#43672,#43673,#43674,#43675,#43676,#43677,#43678,
#43679,#43680,#43681,#43682),(#43683,#43684,#43685,#43686,#43687,#43688,
#43689,#43690,#43691,#43692,#43693,#43694,#43695,#43696,#43697,#43698,#43699)),
 .UNSPECIFIED.,.F.,.F.,.F.,(4,4),(4,1,1,1,1,1,1,1,1,1,1,1,1,1,4),(0.,1.),
(-1.31922727866773E-7,0.0305555555555556,0.0444444444444444,0.114351851851852,
0.184259259259259,0.254166666666666,0.324074074074073,0.39398148148148,
0.463888888888888,0.55324074074074,0.642592592592592,0.731944444444444,
0.821296296296296,0.910648148148148,1.),.UNSPECIFIED.);
#397=PLANE('',#18917);
#398=PLANE('',#18918);
#399=PLANE('',#18919);
#400=PLANE('',#18920);
#1078=(
BOUNDED_SURFACE()
B_SPLINE_SURFACE(5,1,((#41857,#41858),(#41859,#41860),(#41861,#41862),(#41863,
#41864),(#41865,#41866),(#41867,#41868),(#41869,#41870),(#41871,#41872),
(#41873,#41874),(#41875,#41876),(#41877,#41878),(#41879,#41880),(#41881,
#41882),(#41883,#41884),(#41885,#41886),(#41887,#41888),(#41889,#41890),
(#41891,#41892),(#41893,#41894),(#41895,#41896),(#41897,#41898),(#41899,
#41900),(#41901,#41902),(#41903,#41904),(#41905,#41906),(#41907,#41908),
(#41909,#41910),(#41911,#41912),(#41913,#41914),(#41915,#41916),(#41917,
#41918),(#41919,#41920),(#41921,#41922),(#41923,#41924),(#41925,#41926),
(#41927,#41928),(#41929,#41930),(#41931,#41932),(#41933,#41934),(#41935,
#41936),(#41937,#41938),(#41939,#41940),(#41941,#41942),(#41943,#41944),
(#41945,#41946),(#41947,#41948),(#41949,#41950),(#41951,#41952),(#41953,
#41954),(#41955,#41956),(#41957,#41958),(#41959,#41960),(#41961,#41962),
(#41963,#41964),(#41965,#41966),(#41967,#41968),(#41969,#41970),(#41971,
#41972),(#41973,#41974),(#41975,#41976),(#41977,#41978),(#41979,#41980),
(#41981,#41982),(#41983,#41984),(#41985,#41986),(#41987,#41988),(#41989,
#41990),(#41991,#41992),(#41993,#41994),(#41995,#41996),(#41997,#41998),
(#41999,#42000),(#42001,#42002),(#42003,#42004),(#42005,#42006),(#42007,
#42008),(#42009,#42010),(#42011,#42012),(#42013,#42014),(#42015,#42016),
(#42017,#42018),(#42019,#42020),(#42021,#42022),(#42023,#42024),(#42025,
#42026),(#42027,#42028),(#42029,#42030),(#42031,#42032),(#42033,#42034),
(#42035,#42036),(#42037,#42038),(#42039,#42040),(#42041,#42042),(#42043,
#42044),(#42045,#42046),(#42047,#42048),(#42049,#42050),(#42051,#42052),
(#42053,#42054),(#42055,#42056),(#42057,#42058),(#42059,#42060),(#42061,
#42062),(#42063,#42064),(#42065,#42066),(#42067,#42068),(#42069,#42070),
(#42071,#42072),(#42073,#42074),(#42075,#42076),(#42077,#42078),(#42079,
#42080),(#42081,#42082),(#42083,#42084),(#42085,#42086),(#42087,#42088),
(#42089,#42090),(#42091,#42092),(#42093,#42094),(#42095,#42096),(#42097,
#42098),(#42099,#42100),(#42101,#42102),(#42103,#42104),(#42105,#42106),
(#42107,#42108),(#42109,#42110),(#42111,#42112),(#42113,#42114),(#42115,
#42116),(#42117,#42118),(#42119,#42120),(#42121,#42122),(#42123,#42124),
(#42125,#42126),(#42127,#42128),(#42129,#42130),(#42131,#42132),(#42133,
#42134),(#42135,#42136),(#42137,#42138),(#42139,#42140),(#42141,#42142),
(#42143,#42144),(#42145,#42146),(#42147,#42148),(#42149,#42150),(#42151,
#42152),(#42153,#42154),(#42155,#42156),(#42157,#42158),(#42159,#42160),
(#42161,#42162),(#42163,#42164),(#42165,#42166),(#42167,#42168),(#42169,
#42170),(#42171,#42172),(#42173,#42174),(#42175,#42176),(#42177,#42178),
(#42179,#42180),(#42181,#42182),(#42183,#42184),(#42185,#42186),(#42187,
#42188),(#42189,#42190),(#42191,#42192),(#42193,#42194),(#42195,#42196),
(#42197,#42198),(#42199,#42200),(#42201,#42202),(#42203,#42204),(#42205,
#42206),(#42207,#42208),(#42209,#42210),(#42211,#42212),(#42213,#42214),
(#42215,#42216),(#42217,#42218),(#42219,#42220),(#42221,#42222),(#42223,
#42224),(#42225,#42226),(#42227,#42228),(#42229,#42230),(#42231,#42232),
(#42233,#42234),(#42235,#42236),(#42237,#42238),(#42239,#42240),(#42241,
#42242),(#42243,#42244),(#42245,#42246),(#42247,#42248),(#42249,#42250),
(#42251,#42252),(#42253,#42254),(#42255,#42256),(#42257,#42258),(#42259,
#42260),(#42261,#42262),(#42263,#42264),(#42265,#42266),(#42267,#42268),
(#42269,#42270),(#42271,#42272),(#42273,#42274),(#42275,#42276),(#42277,
#42278),(#42279,#42280),(#42281,#42282),(#42283,#42284),(#42285,#42286),
(#42287,#42288),(#42289,#42290),(#42291,#42292),(#42293,#42294),(#42295,
#42296),(#42297,#42298),(#42299,#42300),(#42301,#42302),(#42303,#42304),
(#42305,#42306),(#42307,#42308),(#42309,#42310),(#42311,#42312),(#42313,
#42314),(#42315,#42316),(#42317,#42318),(#42319,#42320),(#42321,#42322),
(#42323,#42324),(#42325,#42326),(#42327,#42328),(#42329,#42330),(#42331,
#42332),(#42333,#42334),(#42335,#42336),(#42337,#42338),(#42339,#42340),
(#42341,#42342),(#42343,#42344),(#42345,#42346),(#42347,#42348),(#42349,
#42350),(#42351,#42352),(#42353,#42354),(#42355,#42356),(#42357,#42358),
(#42359,#42360),(#42361,#42362),(#42363,#42364),(#42365,#42366),(#42367,
#42368),(#42369,#42370),(#42371,#42372),(#42373,#42374),(#42375,#42376),
(#42377,#42378),(#42379,#42380),(#42381,#42382),(#42383,#42384),(#42385,
#42386),(#42387,#42388),(#42389,#42390),(#42391,#42392),(#42393,#42394),
(#42395,#42396),(#42397,#42398),(#42399,#42400),(#42401,#42402),(#42403,
#42404),(#42405,#42406),(#42407,#42408),(#42409,#42410),(#42411,#42412),
(#42413,#42414),(#42415,#42416),(#42417,#42418),(#42419,#42420),(#42421,
#42422),(#42423,#42424),(#42425,#42426),(#42427,#42428),(#42429,#42430),
(#42431,#42432),(#42433,#42434),(#42435,#42436),(#42437,#42438),(#42439,
#42440),(#42441,#42442),(#42443,#42444),(#42445,#42446),(#42447,#42448),
(#42449,#42450),(#42451,#42452),(#42453,#42454),(#42455,#42456),(#42457,
#42458),(#42459,#42460),(#42461,#42462),(#42463,#42464),(#42465,#42466),
(#42467,#42468),(#42469,#42470),(#42471,#42472),(#42473,#42474),(#42475,
#42476),(#42477,#42478),(#42479,#42480),(#42481,#42482),(#42483,#42484),
(#42485,#42486),(#42487,#42488),(#42489,#42490),(#42491,#42492),(#42493,
#42494),(#42495,#42496),(#42497,#42498),(#42499,#42500),(#42501,#42502),
(#42503,#42504),(#42505,#42506),(#42507,#42508),(#42509,#42510),(#42511,
#42512),(#42513,#42514),(#42515,#42516),(#42517,#42518),(#42519,#42520),
(#42521,#42522),(#42523,#42524),(#42525,#42526),(#42527,#42528),(#42529,
#42530),(#42531,#42532),(#42533,#42534),(#42535,#42536),(#42537,#42538),
(#42539,#42540),(#42541,#42542),(#42543,#42544),(#42545,#42546),(#42547,
#42548),(#42549,#42550),(#42551,#42552),(#42553,#42554),(#42555,#42556),
(#42557,#42558),(#42559,#42560),(#42561,#42562),(#42563,#42564),(#42565,
#42566),(#42567,#42568),(#42569,#42570),(#42571,#42572),(#42573,#42574),
(#42575,#42576),(#42577,#42578),(#42579,#42580),(#42581,#42582),(#42583,
#42584),(#42585,#42586)),.UNSPECIFIED.,.F.,.F.,.F.)
B_SPLINE_SURFACE_WITH_KNOTS((6,1,1,1,1,1,1,1,1,1,1,1,1,1,1,1,1,1,1,1,1,
1,1,1,1,1,1,1,1,1,1,1,1,1,1,1,1,1,1,1,1,1,1,1,1,1,1,1,1,1,1,1,1,1,1,1,1,
1,1,1,1,1,1,1,1,1,1,1,1,1,1,1,1,1,1,1,1,1,1,1,1,1,1,1,1,1,1,1,1,1,1,1,1,
1,1,1,1,1,1,1,1,1,1,1,1,1,1,1,1,1,1,1,1,1,1,1,1,1,1,1,1,1,1,1,1,1,1,1,1,
1,1,1,1,1,1,1,1,1,1,1,1,1,1,1,1,1,1,1,1,1,1,1,1,1,1,1,1,1,1,1,1,1,1,1,1,
1,1,1,1,1,1,1,1,1,1,1,1,1,1,1,1,1,1,1,1,1,1,1,1,1,1,1,1,1,1,1,1,1,1,1,1,
1,1,1,1,1,1,1,1,1,1,1,1,1,1,1,1,1,1,1,1,1,1,1,1,1,1,1,1,1,1,1,1,1,1,1,1,
1,1,1,1,1,1,1,1,1,1,1,1,1,1,1,1,1,1,1,1,1,1,1,1,1,1,1,1,1,1,1,1,1,1,1,1,
1,1,1,1,1,1,1,1,1,1,1,1,1,1,1,1,1,1,1,1,1,1,1,1,1,1,1,1,1,1,1,1,1,1,1,1,
1,1,1,1,1,1,1,1,1,1,1,1,1,1,1,1,1,1,1,1,1,1,1,1,1,1,1,1,1,1,1,1,1,1,1,1,
1,1,1,1,1,1,1,1,1,1,1,1,1,1,1,6),(2,2),(0.,0.00277777777777778,0.00555555555555556,
0.00833333333333333,0.0111111111111111,0.0138888888888889,0.0166666666666667,
0.0194444444444444,0.0222222222222222,0.025,0.0277777777777778,0.0305555555555556,
0.0333333333333333,0.0361111111111111,0.0388888888888889,0.0416666666666667,
0.0444444444444444,0.0472222222222222,0.05,0.0527777777777778,0.0555555555555555,
0.0583333333333333,0.0611111111111111,0.0638888888888889,0.0666666666666666,
0.0694444444444444,0.0722222222222222,0.075,0.0777777777777778,0.0805555555555555,
0.0833333333333333,0.0861111111111111,0.0888888888888889,0.0916666666666667,
0.0944444444444445,0.0972222222222222,0.1,0.102777777777778,0.105555555555556,
0.108333333333333,0.111111111111111,0.113888888888889,0.116666666666667,
0.119444444444444,0.122222222222222,0.125,0.127777777777778,0.130555555555556,
0.133333333333333,0.136111111111111,0.138888888888889,0.141666666666667,
0.144444444444444,0.147222222222222,0.15,0.152777777777778,0.155555555555556,
0.158333333333333,0.161111111111111,0.163888888888889,0.166666666666667,
0.169444444444444,0.172222222222222,0.175,0.177777777777778,0.180555555555555,
0.183333333333333,0.186111111111111,0.188888888888889,0.191666666666666,
0.194444444444444,0.197222222222222,0.2,0.202777777777778,0.205555555555555,
0.208333333333333,0.211111111111111,0.213888888888889,0.216666666666666,
0.219444444444444,0.222222222222222,0.225,0.227777777777777,0.230555555555555,
0.233333333333333,0.236111111111111,0.238888888888889,0.241666666666666,
0.244444444444444,0.247222222222222,0.25,0.252777777777777,0.255555555555555,
0.258333333333333,0.261111111111111,0.263888888888888,0.266666666666666,
0.269444444444444,0.272222222222222,0.275,0.277777777777777,0.280555555555555,
0.283333333333333,0.286111111111111,0.288888888888888,0.291666666666666,
0.294444444444444,0.297222222222222,0.299999999999999,0.302777777777777,
0.305555555555555,0.308333333333333,0.311111111111111,0.313888888888888,
0.316666666666666,0.319444444444444,0.322222222222222,0.324999999999999,
0.327777777777777,0.330555555555555,0.333333333333333,0.33611111111111,
0.338888888888888,0.341666666666666,0.344444444444444,0.347222222222221,
0.349999999999999,0.352777777777777,0.355555555555555,0.358333333333333,
0.36111111111111,0.363888888888888,0.366666666666666,0.369444444444444,
0.372222222222221,0.374999999999999,0.377777777777777,0.380555555555555,
0.383333333333332,0.38611111111111,0.388888888888888,0.391666666666666,
0.394444444444444,0.397222222222221,0.399999999999999,0.402777777777777,
0.405555555555555,0.408333333333332,0.41111111111111,0.413888888888888,
0.416666666666666,0.419444444444443,0.422222222222221,0.424999999999999,
0.427777777777777,0.430555555555555,0.433333333333332,0.43611111111111,
0.438888888888888,0.441666666666666,0.444444444444443,0.447222222222221,
0.449999999999999,0.452777777777777,0.455555555555554,0.458333333333332,
0.46111111111111,0.463888888888888,0.466666666666666,0.469444444444443,
0.472222222222221,0.474999999999999,0.477777777777777,0.480555555555554,
0.483333333333332,0.48611111111111,0.488888888888888,0.491666666666665,
0.494444444444443,0.497222222222221,0.499999999999999,0.502777777777777,
0.505555555555554,0.508333333333332,0.51111111111111,0.513888888888888,
0.516666666666665,0.519444444444443,0.522222222222221,0.524999999999999,
0.527777777777776,0.530555555555554,0.533333333333332,0.53611111111111,
0.538888888888888,0.541666666666665,0.544444444444443,0.547222222222221,
0.549999999999999,0.552777777777776,0.555555555555554,0.558333333333332,
0.56111111111111,0.563888888888887,0.566666666666665,0.569444444444443,
0.572222222222221,0.574999999999999,0.577777777777776,0.580555555555554,
0.583333333333332,0.58611111111111,0.588888888888887,0.591666666666665,
0.594444444444443,0.597222222222221,0.599999999999998,0.602777777777776,
0.605555555555554,0.608333333333332,0.611111111111109,0.613888888888887,
0.616666666666665,0.619444444444443,0.622222222222221,0.624999999999998,
0.627777777777776,0.630555555555554,0.633333333333332,0.636111111111109,
0.638888888888887,0.641666666666665,0.644444444444443,0.64722222222222,
0.649999999999998,0.652777777777776,0.655555555555554,0.658333333333332,
0.661111111111109,0.663888888888887,0.666666666666665,0.669444444444443,
0.67222222222222,0.674999999999998,0.677777777777776,0.680555555555554,
0.683333333333331,0.686111111111109,0.688888888888887,0.691666666666665,
0.694444444444443,0.69722222222222,0.699999999999998,0.702777777777776,
0.705555555555554,0.708333333333331,0.711111111111109,0.713888888888887,
0.716666666666665,0.719444444444442,0.72222222222222,0.724999999999998,
0.727777777777776,0.730555555555554,0.733333333333331,0.736111111111109,
0.738888888888887,0.741666666666665,0.744444444444442,0.74722222222222,
0.749999999999998,0.752777777777776,0.755555555555553,0.758333333333331,
0.761111111111109,0.763888888888887,0.766666666666664,0.769444444444442,
0.77222222222222,0.774999999999998,0.777777777777776,0.780555555555553,
0.783333333333331,0.786111111111109,0.788888888888887,0.791666666666664,
0.794444444444442,0.79722222222222,0.799999999999998,0.802777777777775,
0.805555555555553,0.808333333333331,0.811111111111109,0.813888888888887,
0.816666666666664,0.819444444444442,0.82222222222222,0.824999999999998,
0.827777777777775,0.830555555555553,0.833333333333331,0.836111111111109,
0.838888888888886,0.841666666666664,0.844444444444442,0.84722222222222,
0.849999999999998,0.852777777777775,0.855555555555553,0.858333333333331,
0.861111111111109,0.863888888888886,0.866666666666664,0.869444444444442,
0.87222222222222,0.874999999999997,0.877777777777775,0.880555555555553,
0.883333333333331,0.886111111111109,0.888888888888886,0.891666666666664,
0.894444444444442,0.89722222222222,0.899999999999997,0.902777777777775,
0.905555555555553,0.908333333333331,0.911111111111108,0.913888888888886,
0.916666666666664,0.919444444444442,0.92222222222222,0.924999999999997,
0.927777777777775,0.930555555555553,0.933333333333331,0.936111111111108,
0.938888888888886,0.941666666666664,0.944444444444442,0.947222222222219,
0.949999999999997,0.952777777777775,0.955555555555553,0.95833333333333,
0.961111111111108,0.963888888888886,0.966666666666664,0.969444444444442,
0.972222222222219,0.974999999999997,0.977777777777775,0.980555555555553,
0.98333333333333,0.986111111111108,0.988888888888886,0.991666666666664,
0.994444444444441,0.997222222222219,1.),(0.,0.15),.UNSPECIFIED.)
GEOMETRIC_REPRESENTATION_ITEM()
RATIONAL_B_SPLINE_SURFACE(((1.,1.),(1.,1.),(1.,1.),(1.,1.),(1.,1.),(1.,
1.),(1.,1.),(1.,1.),(1.,1.),(1.,1.),(1.,1.),(1.,1.),(1.,1.),(1.,1.),(1.,
1.),(1.,1.),(1.,1.),(1.,1.),(1.,1.),(1.,1.),(1.,1.),(1.,1.),(1.,1.),(1.,
1.),(1.,1.),(1.,1.),(1.,1.),(1.,1.),(1.,1.),(1.,1.),(1.,1.),(1.,1.),(1.,
1.),(1.,1.),(1.,1.),(1.,1.),(1.,1.),(1.,1.),(1.,1.),(1.,1.),(1.,1.),(1.,
1.),(1.,1.),(1.,1.),(1.,1.),(1.,1.),(1.,1.),(1.,1.),(1.,1.),(1.,1.),(1.,
1.),(1.,1.),(1.,1.),(1.,1.),(1.,1.),(1.,1.),(1.,1.),(1.,1.),(1.,1.),(1.,
1.),(1.,1.),(1.,1.),(1.,1.),(1.,1.),(1.,1.),(1.,1.),(1.,1.),(1.,1.),(1.,
1.),(1.,1.),(1.,1.),(1.,1.),(1.,1.),(1.,1.),(1.,1.),(1.,1.),(1.,1.),(1.,
1.),(1.,1.),(1.,1.),(1.,1.),(1.,1.),(1.,1.),(1.,1.),(1.,1.),(1.,1.),(1.,
1.),(1.,1.),(1.,1.),(1.,1.),(1.,1.),(1.,1.),(1.,1.),(1.,1.),(1.,1.),(1.,
1.),(1.,1.),(1.,1.),(1.,1.),(1.,1.),(1.,1.),(1.,1.),(1.,1.),(1.,1.),(1.,
1.),(1.,1.),(1.,1.),(1.,1.),(1.,1.),(1.,1.),(1.,1.),(1.,1.),(1.,1.),(1.,
1.),(1.,1.),(1.,1.),(1.,1.),(1.,1.),(1.,1.),(1.,1.),(1.,1.),(1.,1.),(1.,
1.),(1.,1.),(1.,1.),(1.,1.),(1.,1.),(1.,1.),(1.,1.),(1.,1.),(1.,1.),(1.,
1.),(1.,1.),(1.,1.),(1.,1.),(1.,1.),(1.,1.),(1.,1.),(1.,1.),(1.,1.),(1.,
1.),(1.,1.),(1.,1.),(1.,1.),(1.,1.),(1.,1.),(1.,1.),(1.,1.),(1.,1.),(1.,
1.),(1.,1.),(1.,1.),(1.,1.),(1.,1.),(1.,1.),(1.,1.),(1.,1.),(1.,1.),(1.,
1.),(1.,1.),(1.,1.),(1.,1.),(1.,1.),(1.,1.),(1.,1.),(1.,1.),(1.,1.),(1.,
1.),(1.,1.),(1.,1.),(1.,1.),(1.,1.),(1.,1.),(1.,1.),(1.,1.),(1.,1.),(1.,
1.),(1.,1.),(1.,1.),(1.,1.),(1.,1.),(1.,1.),(1.,1.),(1.,1.),(1.,1.),(1.,
1.),(1.,1.),(1.,1.),(1.,1.),(1.,1.),(1.,1.),(1.,1.),(1.,1.),(1.,1.),(1.,
1.),(1.,1.),(1.,1.),(1.,1.),(1.,1.),(1.,1.),(1.,1.),(1.,1.),(1.,1.),(1.,
1.),(1.,1.),(1.,1.),(1.,1.),(1.,1.),(1.,1.),(1.,1.),(1.,1.),(1.,1.),(1.,
1.),(1.,1.),(1.,1.),(1.,1.),(1.,1.),(1.,1.),(1.,1.),(1.,1.),(1.,1.),(1.,
1.),(1.,1.),(1.,1.),(1.,1.),(1.,1.),(1.,1.),(1.,1.),(1.,1.),(1.,1.),(1.,
1.),(1.,1.),(1.,1.),(1.,1.),(1.,1.),(1.,1.),(1.,1.),(1.,1.),(1.,1.),(1.,
1.),(1.,1.),(1.,1.),(1.,1.),(1.,1.),(1.,1.),(1.,1.),(1.,1.),(1.,1.),(1.,
1.),(1.,1.),(1.,1.),(1.,1.),(1.,1.),(1.,1.),(1.,1.),(1.,1.),(1.,1.),(1.,
1.),(1.,1.),(1.,1.),(1.,1.),(1.,1.),(1.,1.),(1.,1.),(1.,1.),(1.,1.),(1.,
1.),(1.,1.),(1.,1.),(1.,1.),(1.,1.),(1.,1.),(1.,1.),(1.,1.),(1.,1.),(1.,
1.),(1.,1.),(1.,1.),(1.,1.),(1.,1.),(1.,1.),(1.,1.),(1.,1.),(1.,1.),(1.,
1.),(1.,1.),(1.,1.),(1.,1.),(1.,1.),(1.,1.),(1.,1.),(1.,1.),(1.,1.),(1.,
1.),(1.,1.),(1.,1.),(1.,1.),(1.,1.),(1.,1.),(1.,1.),(1.,1.),(1.,1.),(1.,
1.),(1.,1.),(1.,1.),(1.,1.),(1.,1.),(1.,1.),(1.,1.),(1.,1.),(1.,1.),(1.,
1.),(1.,1.),(1.,1.),(1.,1.),(1.,1.),(1.,1.),(1.,1.),(1.,1.),(1.,1.),(1.,
1.),(1.,1.),(1.,1.),(1.,1.),(1.,1.),(1.,1.),(1.,1.),(1.,1.),(1.,1.),(1.,
1.),(1.,1.),(1.,1.),(1.,1.),(1.,1.),(1.,1.),(1.,1.),(1.,1.),(1.,1.),(1.,
1.),(1.,1.),(1.,1.),(1.,1.),(1.,1.),(1.,1.),(1.,1.),(1.,1.),(1.,1.),(1.,
1.),(1.,1.),(1.,1.),(1.,1.),(1.,1.),(1.,1.),(1.,1.),(1.,1.),(1.,1.),(1.,
1.),(1.,1.),(1.,1.),(1.,1.),(1.,1.),(1.,1.),(1.,1.),(1.,1.),(1.,1.)))
REPRESENTATION_ITEM('')
SURFACE()
);
#1079=(
BOUNDED_SURFACE()
B_SPLINE_SURFACE(5,1,((#42883,#42884),(#42885,#42886),(#42887,#42888),(#42889,
#42890),(#42891,#42892),(#42893,#42894),(#42895,#42896),(#42897,#42898),
(#42899,#42900),(#42901,#42902),(#42903,#42904),(#42905,#42906),(#42907,
#42908),(#42909,#42910),(#42911,#42912),(#42913,#42914),(#42915,#42916),
(#42917,#42918),(#42919,#42920),(#42921,#42922),(#42923,#42924),(#42925,
#42926),(#42927,#42928),(#42929,#42930),(#42931,#42932),(#42933,#42934),
(#42935,#42936),(#42937,#42938),(#42939,#42940),(#42941,#42942),(#42943,
#42944),(#42945,#42946),(#42947,#42948),(#42949,#42950),(#42951,#42952),
(#42953,#42954),(#42955,#42956),(#42957,#42958),(#42959,#42960),(#42961,
#42962),(#42963,#42964),(#42965,#42966),(#42967,#42968),(#42969,#42970),
(#42971,#42972),(#42973,#42974),(#42975,#42976),(#42977,#42978),(#42979,
#42980),(#42981,#42982),(#42983,#42984),(#42985,#42986),(#42987,#42988),
(#42989,#42990),(#42991,#42992),(#42993,#42994),(#42995,#42996),(#42997,
#42998),(#42999,#43000),(#43001,#43002),(#43003,#43004),(#43005,#43006),
(#43007,#43008),(#43009,#43010),(#43011,#43012),(#43013,#43014),(#43015,
#43016),(#43017,#43018),(#43019,#43020),(#43021,#43022),(#43023,#43024),
(#43025,#43026),(#43027,#43028),(#43029,#43030),(#43031,#43032),(#43033,
#43034),(#43035,#43036),(#43037,#43038),(#43039,#43040),(#43041,#43042),
(#43043,#43044),(#43045,#43046),(#43047,#43048),(#43049,#43050),(#43051,
#43052),(#43053,#43054),(#43055,#43056),(#43057,#43058),(#43059,#43060),
(#43061,#43062),(#43063,#43064),(#43065,#43066),(#43067,#43068),(#43069,
#43070),(#43071,#43072),(#43073,#43074),(#43075,#43076),(#43077,#43078),
(#43079,#43080),(#43081,#43082),(#43083,#43084),(#43085,#43086),(#43087,
#43088),(#43089,#43090),(#43091,#43092),(#43093,#43094),(#43095,#43096),
(#43097,#43098),(#43099,#43100),(#43101,#43102),(#43103,#43104),(#43105,
#43106),(#43107,#43108),(#43109,#43110),(#43111,#43112),(#43113,#43114),
(#43115,#43116),(#43117,#43118),(#43119,#43120),(#43121,#43122),(#43123,
#43124),(#43125,#43126),(#43127,#43128),(#43129,#43130),(#43131,#43132),
(#43133,#43134),(#43135,#43136),(#43137,#43138),(#43139,#43140),(#43141,
#43142),(#43143,#43144),(#43145,#43146),(#43147,#43148),(#43149,#43150),
(#43151,#43152),(#43153,#43154),(#43155,#43156),(#43157,#43158),(#43159,
#43160),(#43161,#43162),(#43163,#43164),(#43165,#43166),(#43167,#43168),
(#43169,#43170),(#43171,#43172),(#43173,#43174),(#43175,#43176),(#43177,
#43178),(#43179,#43180),(#43181,#43182),(#43183,#43184),(#43185,#43186),
(#43187,#43188),(#43189,#43190),(#43191,#43192),(#43193,#43194),(#43195,
#43196),(#43197,#43198),(#43199,#43200),(#43201,#43202),(#43203,#43204),
(#43205,#43206),(#43207,#43208),(#43209,#43210),(#43211,#43212),(#43213,
#43214),(#43215,#43216),(#43217,#43218),(#43219,#43220),(#43221,#43222),
(#43223,#43224),(#43225,#43226),(#43227,#43228),(#43229,#43230),(#43231,
#43232),(#43233,#43234),(#43235,#43236),(#43237,#43238),(#43239,#43240),
(#43241,#43242),(#43243,#43244),(#43245,#43246),(#43247,#43248),(#43249,
#43250),(#43251,#43252),(#43253,#43254),(#43255,#43256),(#43257,#43258),
(#43259,#43260),(#43261,#43262),(#43263,#43264),(#43265,#43266),(#43267,
#43268),(#43269,#43270),(#43271,#43272),(#43273,#43274),(#43275,#43276),
(#43277,#43278),(#43279,#43280),(#43281,#43282),(#43283,#43284),(#43285,
#43286),(#43287,#43288),(#43289,#43290),(#43291,#43292),(#43293,#43294),
(#43295,#43296),(#43297,#43298),(#43299,#43300),(#43301,#43302),(#43303,
#43304),(#43305,#43306),(#43307,#43308),(#43309,#43310),(#43311,#43312),
(#43313,#43314),(#43315,#43316),(#43317,#43318),(#43319,#43320),(#43321,
#43322),(#43323,#43324),(#43325,#43326),(#43327,#43328),(#43329,#43330),
(#43331,#43332),(#43333,#43334),(#43335,#43336),(#43337,#43338),(#43339,
#43340),(#43341,#43342),(#43343,#43344),(#43345,#43346),(#43347,#43348),
(#43349,#43350),(#43351,#43352),(#43353,#43354),(#43355,#43356),(#43357,
#43358),(#43359,#43360),(#43361,#43362),(#43363,#43364),(#43365,#43366),
(#43367,#43368),(#43369,#43370),(#43371,#43372),(#43373,#43374),(#43375,
#43376),(#43377,#43378),(#43379,#43380),(#43381,#43382),(#43383,#43384),
(#43385,#43386),(#43387,#43388),(#43389,#43390),(#43391,#43392),(#43393,
#43394),(#43395,#43396),(#43397,#43398),(#43399,#43400),(#43401,#43402),
(#43403,#43404),(#43405,#43406),(#43407,#43408),(#43409,#43410),(#43411,
#43412),(#43413,#43414),(#43415,#43416),(#43417,#43418),(#43419,#43420),
(#43421,#43422),(#43423,#43424),(#43425,#43426),(#43427,#43428),(#43429,
#43430),(#43431,#43432),(#43433,#43434),(#43435,#43436),(#43437,#43438),
(#43439,#43440),(#43441,#43442),(#43443,#43444),(#43445,#43446),(#43447,
#43448),(#43449,#43450),(#43451,#43452),(#43453,#43454),(#43455,#43456),
(#43457,#43458),(#43459,#43460),(#43461,#43462),(#43463,#43464),(#43465,
#43466),(#43467,#43468),(#43469,#43470),(#43471,#43472),(#43473,#43474),
(#43475,#43476),(#43477,#43478),(#43479,#43480),(#43481,#43482),(#43483,
#43484),(#43485,#43486),(#43487,#43488),(#43489,#43490),(#43491,#43492),
(#43493,#43494),(#43495,#43496),(#43497,#43498),(#43499,#43500),(#43501,
#43502),(#43503,#43504),(#43505,#43506),(#43507,#43508),(#43509,#43510),
(#43511,#43512),(#43513,#43514),(#43515,#43516),(#43517,#43518),(#43519,
#43520),(#43521,#43522),(#43523,#43524),(#43525,#43526),(#43527,#43528),
(#43529,#43530),(#43531,#43532),(#43533,#43534),(#43535,#43536),(#43537,
#43538),(#43539,#43540),(#43541,#43542),(#43543,#43544),(#43545,#43546),
(#43547,#43548),(#43549,#43550),(#43551,#43552),(#43553,#43554),(#43555,
#43556),(#43557,#43558),(#43559,#43560),(#43561,#43562),(#43563,#43564),
(#43565,#43566),(#43567,#43568),(#43569,#43570),(#43571,#43572),(#43573,
#43574),(#43575,#43576),(#43577,#43578),(#43579,#43580),(#43581,#43582),
(#43583,#43584),(#43585,#43586),(#43587,#43588),(#43589,#43590),(#43591,
#43592),(#43593,#43594),(#43595,#43596),(#43597,#43598),(#43599,#43600),
(#43601,#43602),(#43603,#43604),(#43605,#43606),(#43607,#43608),(#43609,
#43610),(#43611,#43612)),.UNSPECIFIED.,.F.,.F.,.F.)
B_SPLINE_SURFACE_WITH_KNOTS((6,1,1,1,1,1,1,1,1,1,1,1,1,1,1,1,1,1,1,1,1,
1,1,1,1,1,1,1,1,1,1,1,1,1,1,1,1,1,1,1,1,1,1,1,1,1,1,1,1,1,1,1,1,1,1,1,1,
1,1,1,1,1,1,1,1,1,1,1,1,1,1,1,1,1,1,1,1,1,1,1,1,1,1,1,1,1,1,1,1,1,1,1,1,
1,1,1,1,1,1,1,1,1,1,1,1,1,1,1,1,1,1,1,1,1,1,1,1,1,1,1,1,1,1,1,1,1,1,1,1,
1,1,1,1,1,1,1,1,1,1,1,1,1,1,1,1,1,1,1,1,1,1,1,1,1,1,1,1,1,1,1,1,1,1,1,1,
1,1,1,1,1,1,1,1,1,1,1,1,1,1,1,1,1,1,1,1,1,1,1,1,1,1,1,1,1,1,1,1,1,1,1,1,
1,1,1,1,1,1,1,1,1,1,1,1,1,1,1,1,1,1,1,1,1,1,1,1,1,1,1,1,1,1,1,1,1,1,1,1,
1,1,1,1,1,1,1,1,1,1,1,1,1,1,1,1,1,1,1,1,1,1,1,1,1,1,1,1,1,1,1,1,1,1,1,1,
1,1,1,1,1,1,1,1,1,1,1,1,1,1,1,1,1,1,1,1,1,1,1,1,1,1,1,1,1,1,1,1,1,1,1,1,
1,1,1,1,1,1,1,1,1,1,1,1,1,1,1,1,1,1,1,1,1,1,1,1,1,1,1,1,1,1,1,1,1,1,1,1,
1,1,1,1,1,1,1,1,1,1,1,1,1,1,1,6),(2,2),(0.,0.00277777777777778,0.00555555555555556,
0.00833333333333333,0.0111111111111111,0.0138888888888889,0.0166666666666667,
0.0194444444444444,0.0222222222222222,0.025,0.0277777777777778,0.0305555555555556,
0.0333333333333333,0.0361111111111111,0.0388888888888889,0.0416666666666667,
0.0444444444444444,0.0472222222222222,0.05,0.0527777777777778,0.0555555555555555,
0.0583333333333333,0.0611111111111111,0.0638888888888889,0.0666666666666666,
0.0694444444444444,0.0722222222222222,0.075,0.0777777777777778,0.0805555555555555,
0.0833333333333333,0.0861111111111111,0.0888888888888889,0.0916666666666667,
0.0944444444444445,0.0972222222222222,0.1,0.102777777777778,0.105555555555556,
0.108333333333333,0.111111111111111,0.113888888888889,0.116666666666667,
0.119444444444444,0.122222222222222,0.125,0.127777777777778,0.130555555555556,
0.133333333333333,0.136111111111111,0.138888888888889,0.141666666666667,
0.144444444444444,0.147222222222222,0.15,0.152777777777778,0.155555555555556,
0.158333333333333,0.161111111111111,0.163888888888889,0.166666666666667,
0.169444444444444,0.172222222222222,0.175,0.177777777777778,0.180555555555555,
0.183333333333333,0.186111111111111,0.188888888888889,0.191666666666666,
0.194444444444444,0.197222222222222,0.2,0.202777777777778,0.205555555555555,
0.208333333333333,0.211111111111111,0.213888888888889,0.216666666666666,
0.219444444444444,0.222222222222222,0.225,0.227777777777777,0.230555555555555,
0.233333333333333,0.236111111111111,0.238888888888889,0.241666666666666,
0.244444444444444,0.247222222222222,0.25,0.252777777777777,0.255555555555555,
0.258333333333333,0.261111111111111,0.263888888888888,0.266666666666666,
0.269444444444444,0.272222222222222,0.275,0.277777777777777,0.280555555555555,
0.283333333333333,0.286111111111111,0.288888888888888,0.291666666666666,
0.294444444444444,0.297222222222222,0.299999999999999,0.302777777777777,
0.305555555555555,0.308333333333333,0.311111111111111,0.313888888888888,
0.316666666666666,0.319444444444444,0.322222222222222,0.324999999999999,
0.327777777777777,0.330555555555555,0.333333333333333,0.33611111111111,
0.338888888888888,0.341666666666666,0.344444444444444,0.347222222222221,
0.349999999999999,0.352777777777777,0.355555555555555,0.358333333333333,
0.36111111111111,0.363888888888888,0.366666666666666,0.369444444444444,
0.372222222222221,0.374999999999999,0.377777777777777,0.380555555555555,
0.383333333333332,0.38611111111111,0.388888888888888,0.391666666666666,
0.394444444444444,0.397222222222221,0.399999999999999,0.402777777777777,
0.405555555555555,0.408333333333332,0.41111111111111,0.413888888888888,
0.416666666666666,0.419444444444443,0.422222222222221,0.424999999999999,
0.427777777777777,0.430555555555555,0.433333333333332,0.43611111111111,
0.438888888888888,0.441666666666666,0.444444444444443,0.447222222222221,
0.449999999999999,0.452777777777777,0.455555555555554,0.458333333333332,
0.46111111111111,0.463888888888888,0.466666666666666,0.469444444444443,
0.472222222222221,0.474999999999999,0.477777777777777,0.480555555555554,
0.483333333333332,0.48611111111111,0.488888888888888,0.491666666666665,
0.494444444444443,0.497222222222221,0.499999999999999,0.502777777777777,
0.505555555555554,0.508333333333332,0.51111111111111,0.513888888888888,
0.516666666666665,0.519444444444443,0.522222222222221,0.524999999999999,
0.527777777777776,0.530555555555554,0.533333333333332,0.53611111111111,
0.538888888888888,0.541666666666665,0.544444444444443,0.547222222222221,
0.549999999999999,0.552777777777776,0.555555555555554,0.558333333333332,
0.56111111111111,0.563888888888887,0.566666666666665,0.569444444444443,
0.572222222222221,0.574999999999999,0.577777777777776,0.580555555555554,
0.583333333333332,0.58611111111111,0.588888888888887,0.591666666666665,
0.594444444444443,0.597222222222221,0.599999999999998,0.602777777777776,
0.605555555555554,0.608333333333332,0.611111111111109,0.613888888888887,
0.616666666666665,0.619444444444443,0.622222222222221,0.624999999999998,
0.627777777777776,0.630555555555554,0.633333333333332,0.636111111111109,
0.638888888888887,0.641666666666665,0.644444444444443,0.64722222222222,
0.649999999999998,0.652777777777776,0.655555555555554,0.658333333333332,
0.661111111111109,0.663888888888887,0.666666666666665,0.669444444444443,
0.67222222222222,0.674999999999998,0.677777777777776,0.680555555555554,
0.683333333333331,0.686111111111109,0.688888888888887,0.691666666666665,
0.694444444444443,0.69722222222222,0.699999999999998,0.702777777777776,
0.705555555555554,0.708333333333331,0.711111111111109,0.713888888888887,
0.716666666666665,0.719444444444442,0.72222222222222,0.724999999999998,
0.727777777777776,0.730555555555554,0.733333333333331,0.736111111111109,
0.738888888888887,0.741666666666665,0.744444444444442,0.74722222222222,
0.749999999999998,0.752777777777776,0.755555555555553,0.758333333333331,
0.761111111111109,0.763888888888887,0.766666666666664,0.769444444444442,
0.77222222222222,0.774999999999998,0.777777777777776,0.780555555555553,
0.783333333333331,0.786111111111109,0.788888888888887,0.791666666666664,
0.794444444444442,0.79722222222222,0.799999999999998,0.802777777777775,
0.805555555555553,0.808333333333331,0.811111111111109,0.813888888888887,
0.816666666666664,0.819444444444442,0.82222222222222,0.824999999999998,
0.827777777777775,0.830555555555553,0.833333333333331,0.836111111111109,
0.838888888888886,0.841666666666664,0.844444444444442,0.84722222222222,
0.849999999999998,0.852777777777775,0.855555555555553,0.858333333333331,
0.861111111111109,0.863888888888886,0.866666666666664,0.869444444444442,
0.87222222222222,0.874999999999997,0.877777777777775,0.880555555555553,
0.883333333333331,0.886111111111109,0.888888888888886,0.891666666666664,
0.894444444444442,0.89722222222222,0.899999999999997,0.902777777777775,
0.905555555555553,0.908333333333331,0.911111111111108,0.913888888888886,
0.916666666666664,0.919444444444442,0.92222222222222,0.924999999999997,
0.927777777777775,0.930555555555553,0.933333333333331,0.936111111111108,
0.938888888888886,0.941666666666664,0.944444444444442,0.947222222222219,
0.949999999999997,0.952777777777775,0.955555555555553,0.95833333333333,
0.961111111111108,0.963888888888886,0.966666666666664,0.969444444444442,
0.972222222222219,0.974999999999997,0.977777777777775,0.980555555555553,
0.98333333333333,0.986111111111108,0.988888888888886,0.991666666666664,
0.994444444444441,0.997222222222219,1.),(0.,0.15),.UNSPECIFIED.)
GEOMETRIC_REPRESENTATION_ITEM()
RATIONAL_B_SPLINE_SURFACE(((1.,1.),(1.,1.),(1.,1.),(1.,1.),(1.,1.),(1.,
1.),(1.,1.),(1.,1.),(1.,1.),(1.,1.),(1.,1.),(1.,1.),(1.,1.),(1.,1.),(1.,
1.),(1.,1.),(1.,1.),(1.,1.),(1.,1.),(1.,1.),(1.,1.),(1.,1.),(1.,1.),(1.,
1.),(1.,1.),(1.,1.),(1.,1.),(1.,1.),(1.,1.),(1.,1.),(1.,1.),(1.,1.),(1.,
1.),(1.,1.),(1.,1.),(1.,1.),(1.,1.),(1.,1.),(1.,1.),(1.,1.),(1.,1.),(1.,
1.),(1.,1.),(1.,1.),(1.,1.),(1.,1.),(1.,1.),(1.,1.),(1.,1.),(1.,1.),(1.,
1.),(1.,1.),(1.,1.),(1.,1.),(1.,1.),(1.,1.),(1.,1.),(1.,1.),(1.,1.),(1.,
1.),(1.,1.),(1.,1.),(1.,1.),(1.,1.),(1.,1.),(1.,1.),(1.,1.),(1.,1.),(1.,
1.),(1.,1.),(1.,1.),(1.,1.),(1.,1.),(1.,1.),(1.,1.),(1.,1.),(1.,1.),(1.,
1.),(1.,1.),(1.,1.),(1.,1.),(1.,1.),(1.,1.),(1.,1.),(1.,1.),(1.,1.),(1.,
1.),(1.,1.),(1.,1.),(1.,1.),(1.,1.),(1.,1.),(1.,1.),(1.,1.),(1.,1.),(1.,
1.),(1.,1.),(1.,1.),(1.,1.),(1.,1.),(1.,1.),(1.,1.),(1.,1.),(1.,1.),(1.,
1.),(1.,1.),(1.,1.),(1.,1.),(1.,1.),(1.,1.),(1.,1.),(1.,1.),(1.,1.),(1.,
1.),(1.,1.),(1.,1.),(1.,1.),(1.,1.),(1.,1.),(1.,1.),(1.,1.),(1.,1.),(1.,
1.),(1.,1.),(1.,1.),(1.,1.),(1.,1.),(1.,1.),(1.,1.),(1.,1.),(1.,1.),(1.,
1.),(1.,1.),(1.,1.),(1.,1.),(1.,1.),(1.,1.),(1.,1.),(1.,1.),(1.,1.),(1.,
1.),(1.,1.),(1.,1.),(1.,1.),(1.,1.),(1.,1.),(1.,1.),(1.,1.),(1.,1.),(1.,
1.),(1.,1.),(1.,1.),(1.,1.),(1.,1.),(1.,1.),(1.,1.),(1.,1.),(1.,1.),(1.,
1.),(1.,1.),(1.,1.),(1.,1.),(1.,1.),(1.,1.),(1.,1.),(1.,1.),(1.,1.),(1.,
1.),(1.,1.),(1.,1.),(1.,1.),(1.,1.),(1.,1.),(1.,1.),(1.,1.),(1.,1.),(1.,
1.),(1.,1.),(1.,1.),(1.,1.),(1.,1.),(1.,1.),(1.,1.),(1.,1.),(1.,1.),(1.,
1.),(1.,1.),(1.,1.),(1.,1.),(1.,1.),(1.,1.),(1.,1.),(1.,1.),(1.,1.),(1.,
1.),(1.,1.),(1.,1.),(1.,1.),(1.,1.),(1.,1.),(1.,1.),(1.,1.),(1.,1.),(1.,
1.),(1.,1.),(1.,1.),(1.,1.),(1.,1.),(1.,1.),(1.,1.),(1.,1.),(1.,1.),(1.,
1.),(1.,1.),(1.,1.),(1.,1.),(1.,1.),(1.,1.),(1.,1.),(1.,1.),(1.,1.),(1.,
1.),(1.,1.),(1.,1.),(1.,1.),(1.,1.),(1.,1.),(1.,1.),(1.,1.),(1.,1.),(1.,
1.),(1.,1.),(1.,1.),(1.,1.),(1.,1.),(1.,1.),(1.,1.),(1.,1.),(1.,1.),(1.,
1.),(1.,1.),(1.,1.),(1.,1.),(1.,1.),(1.,1.),(1.,1.),(1.,1.),(1.,1.),(1.,
1.),(1.,1.),(1.,1.),(1.,1.),(1.,1.),(1.,1.),(1.,1.),(1.,1.),(1.,1.),(1.,
1.),(1.,1.),(1.,1.),(1.,1.),(1.,1.),(1.,1.),(1.,1.),(1.,1.),(1.,1.),(1.,
1.),(1.,1.),(1.,1.),(1.,1.),(1.,1.),(1.,1.),(1.,1.),(1.,1.),(1.,1.),(1.,
1.),(1.,1.),(1.,1.),(1.,1.),(1.,1.),(1.,1.),(1.,1.),(1.,1.),(1.,1.),(1.,
1.),(1.,1.),(1.,1.),(1.,1.),(1.,1.),(1.,1.),(1.,1.),(1.,1.),(1.,1.),(1.,
1.),(1.,1.),(1.,1.),(1.,1.),(1.,1.),(1.,1.),(1.,1.),(1.,1.),(1.,1.),(1.,
1.),(1.,1.),(1.,1.),(1.,1.),(1.,1.),(1.,1.),(1.,1.),(1.,1.),(1.,1.),(1.,
1.),(1.,1.),(1.,1.),(1.,1.),(1.,1.),(1.,1.),(1.,1.),(1.,1.),(1.,1.),(1.,
1.),(1.,1.),(1.,1.),(1.,1.),(1.,1.),(1.,1.),(1.,1.),(1.,1.),(1.,1.),(1.,
1.),(1.,1.),(1.,1.),(1.,1.),(1.,1.),(1.,1.),(1.,1.),(1.,1.),(1.,1.),(1.,
1.),(1.,1.),(1.,1.),(1.,1.),(1.,1.),(1.,1.),(1.,1.),(1.,1.),(1.,1.),(1.,
1.),(1.,1.),(1.,1.),(1.,1.),(1.,1.),(1.,1.),(1.,1.),(1.,1.),(1.,1.),(1.,
1.),(1.,1.),(1.,1.),(1.,1.),(1.,1.),(1.,1.),(1.,1.),(1.,1.),(1.,1.)))
REPRESENTATION_ITEM('')
SURFACE()
);
#1296=STYLED_ITEM('',(#60520),#88);
#1632=FACE_OUTER_BOUND('',#2605,.T.);
#1633=FACE_OUTER_BOUND('',#2606,.T.);
#1634=FACE_OUTER_BOUND('',#2607,.T.);
#1635=FACE_OUTER_BOUND('',#2608,.T.);
#1636=FACE_OUTER_BOUND('',#2609,.T.);
#1637=FACE_OUTER_BOUND('',#2610,.T.);
#1638=FACE_OUTER_BOUND('',#2611,.T.);
#1639=FACE_OUTER_BOUND('',#2612,.T.);
#1640=FACE_OUTER_BOUND('',#2613,.T.);
#1641=FACE_OUTER_BOUND('',#2614,.T.);
#2605=EDGE_LOOP('',(#13675,#13676,#13677,#13678));
#2606=EDGE_LOOP('',(#13679,#13680,#13681,#13682,#13683,#13684,#13685,#13686));
#2607=EDGE_LOOP('',(#13687,#13688,#13689,#13690));
#2608=EDGE_LOOP('',(#13691,#13692,#13693,#13694));
#2609=EDGE_LOOP('',(#13695,#13696,#13697,#13698));
#2610=EDGE_LOOP('',(#13699,#13700,#13701,#13702));
#2611=EDGE_LOOP('',(#13703,#13704,#13705,#13706));
#2612=EDGE_LOOP('',(#13707,#13708,#13709,#13710,#13711,#13712,#13713,#13714));
#2613=EDGE_LOOP('',(#13715,#13716,#13717,#13718));
#2614=EDGE_LOOP('',(#13719,#13720,#13721,#13722));
#4080=B_SPLINE_CURVE_WITH_KNOTS('',3,(#41786,#41787,#41788,#41789),
 .UNSPECIFIED.,.F.,.F.,(4,4),(-1.,0.),.UNSPECIFIED.);
#4081=B_SPLINE_CURVE_WITH_KNOTS('',3,(#41791,#41792,#41793,#41794,#41795,
#41796,#41797,#41798,#41799,#41800,#41801,#41802,#41803,#41804,#41805,#41806,
#41807),.UNSPECIFIED.,.F.,.F.,(4,1,1,1,1,1,1,1,1,1,1,1,1,1,4),(-0.999999887132374,
-0.928571428571429,-0.857142857142857,-0.785714285714286,-0.714285714285714,
-0.619047619047619,-0.571428571428571,-0.476190476190476,-0.428571428571429,
-0.357142857142857,-0.285714285714286,-0.214285714285714,-0.142857142857143,
-0.0714285714285714,-2.25735216844453E-7),.UNSPECIFIED.);
#4082=B_SPLINE_CURVE_WITH_KNOTS('',3,(#41809,#41810,#41811,#41812),
 .UNSPECIFIED.,.F.,.F.,(4,4),(0.,0.0212132034460131),.UNSPECIFIED.);
#4083=B_SPLINE_CURVE_WITH_KNOTS('',3,(#41813,#41814,#41815,#41816,#41817,
#41818,#41819,#41820,#41821,#41822,#41823,#41824,#41825,#41826,#41827,#41828,
#41829),.UNSPECIFIED.,.F.,.F.,(4,1,1,1,1,1,1,1,1,1,1,1,1,1,4),(0.,0.0714285714285714,
0.142857142857143,0.214285714285714,0.285714285714286,0.357142857142857,
0.428571428571429,0.476190476190476,0.571428571428571,0.619047619047619,
0.714285714285714,0.785714285714286,0.857142857142857,0.928571428571429,
1.),.UNSPECIFIED.);
#4084=B_SPLINE_CURVE_WITH_KNOTS('',3,(#41834,#41835,#41836,#41837),
 .UNSPECIFIED.,.F.,.F.,(4,4),(-1.,0.),.UNSPECIFIED.);
#4085=B_SPLINE_CURVE_WITH_KNOTS('',3,(#41841,#41842,#41843,#41844,#41845,
#41846),.UNSPECIFIED.,.F.,.F.,(4,2,4),(0.,0.0106066017229243,0.0212132034458491),
 .UNSPECIFIED.);
#4086=B_SPLINE_CURVE_WITH_KNOTS('',3,(#41850,#41851,#41852,#41853,#41854,
#41855),.UNSPECIFIED.,.F.,.F.,(4,2,4),(0.,0.0106066017229245,0.0212132034458491),
 .UNSPECIFIED.);
#4087=B_SPLINE_CURVE_WITH_KNOTS('',3,(#42589,#42590,#42591,#42592,#42593,
#42594,#42595,#42596,#42597,#42598,#42599,#42600,#42601,#42602,#42603,#42604,
#42605),.UNSPECIFIED.,.F.,.F.,(4,1,1,1,1,1,1,1,1,1,1,1,1,1,4),(-0.99999988713236,
-0.928571323765762,-0.857142760399165,-0.785714197032568,-0.71428563366597,
-0.642857070299373,-0.571428506932776,-0.523809464688377,-0.428571380199581,
-0.380952337955183,-0.285714253466386,-0.214285690099789,-0.142857126733191,
-0.071428563366594,3.39227166254691E-15),.UNSPECIFIED.);
#4088=B_SPLINE_CURVE_WITH_KNOTS('',3,(#42675,#42676,#42677,#42678),
 .UNSPECIFIED.,.F.,.F.,(4,4),(0.,0.021213203446013),.UNSPECIFIED.);
#4089=B_SPLINE_CURVE_WITH_KNOTS('',3,(#42679,#42680,#42681,#42682,#42683,
#42684,#42685,#42686,#42687,#42688,#42689,#42690,#42691,#42692,#42693,#42694,
#42695),.UNSPECIFIED.,.F.,.F.,(4,1,1,1,1,1,1,1,1,1,1,1,1,1,4),(1.12867617307888E-7,
0.071428563366594,0.142857126733191,0.214285690099789,0.285714253466386,
0.380952337955183,0.428571380199581,0.523809464688377,0.571428506932776,
0.642857070299373,0.71428563366597,0.785714197032568,0.857142760399165,
0.928571323765762,0.99999988713236),.UNSPECIFIED.);
#4090=B_SPLINE_CURVE_WITH_KNOTS('',3,(#42842,#42843,#42844,#42845,#42846,
#42847,#42848,#42849,#42850),.UNSPECIFIED.,.F.,.F.,(4,1,1,1,1,1,4),(-1.,
-0.285714285714286,-0.142857142857143,-0.107142857142857,-0.0714285714285714,
-0.0357142857142857,0.),.UNSPECIFIED.);
#4091=B_SPLINE_CURVE_WITH_KNOTS('',3,(#42851,#42852,#42853,#42854,#42855,
#42856,#42857,#42858,#42859,#42860,#42861,#42862,#42863,#42864,#42865,#42866),
 .UNSPECIFIED.,.F.,.F.,(4,1,1,1,1,1,1,1,1,1,1,1,1,4),(-1.,-0.910648148148148,
-0.821296296296296,-0.731944444444444,-0.642592592592592,-0.55324074074074,
-0.463888888888888,-0.39398148148148,-0.324074074074073,-0.254166666666666,
-0.184259259259259,-0.114351851851852,-0.0444444444444444,1.31922727866773E-7),
 .UNSPECIFIED.);
#4092=B_SPLINE_CURVE_WITH_KNOTS('',3,(#42867,#42868,#42869,#42870,#42871,
#42872,#42873,#42874,#42875,#42876,#42877,#42878,#42879,#42880,#42881,#42882),
 .UNSPECIFIED.,.F.,.F.,(4,1,1,1,1,1,1,1,1,1,1,1,1,4),(0.,0.0444444444444444,
0.114351851851852,0.184259259259259,0.254166666666666,0.324074074074073,
0.39398148148148,0.463888888888888,0.55324074074074,0.642592592592592,0.731944444444444,
0.821296296296296,0.910648148148148,1.),.UNSPECIFIED.);
#4093=B_SPLINE_CURVE_WITH_KNOTS('',3,(#43614,#43615,#43616,#43617,#43618,
#43619,#43620,#43621,#43622,#43623,#43624,#43625,#43626,#43627,#43628,#43629,
#43630),.UNSPECIFIED.,.F.,.F.,(4,1,1,1,1,1,1,1,1,1,1,1,1,1,4),(-1.,-0.910648148148148,
-0.821296296296296,-0.731944444444444,-0.642592592592592,-0.55324074074074,
-0.463888888888888,-0.39398148148148,-0.324074074074073,-0.254166666666666,
-0.184259259259259,-0.114351851851852,-0.0444444444444444,-0.0305555555555556,
-1.31922710467803E-7),.UNSPECIFIED.);
#4094=B_SPLINE_CURVE_WITH_KNOTS('',3,(#43701,#43702,#43703,#43704),
 .UNSPECIFIED.,.F.,.F.,(4,4),(-1.,0.),.UNSPECIFIED.);
#4095=B_SPLINE_CURVE_WITH_KNOTS('',3,(#43705,#43706,#43707,#43708,#43709,
#43710,#43711,#43712,#43713,#43714,#43715,#43716,#43717,#43718,#43719,#43720,
#43721),.UNSPECIFIED.,.F.,.F.,(4,1,1,1,1,1,1,1,1,1,1,1,1,1,4),(-1.31922727866773E-7,
0.0305555555555556,0.0444444444444444,0.114351851851852,0.184259259259259,
0.254166666666666,0.324074074074073,0.39398148148148,0.463888888888888,
0.55324074074074,0.642592592592592,0.731944444444444,0.821296296296296,
0.910648148148148,1.),.UNSPECIFIED.);
#4772=LINE('',#41832,#6184);
#4773=LINE('',#41839,#6185);
#4774=LINE('',#41848,#6186);
#4775=LINE('',#41856,#6187);
#4776=LINE('',#42588,#6188);
#4777=LINE('',#43631,#6189);
#4778=LINE('',#43723,#6190);
#4779=LINE('',#43724,#6191);
#6184=VECTOR('',#20950,10.);
#6185=VECTOR('',#20951,10.);
#6186=VECTOR('',#20952,10.);
#6187=VECTOR('',#20953,10.);
#6188=VECTOR('',#20954,10.);
#6189=VECTOR('',#20955,10.);
#6190=VECTOR('',#20958,10.);
#6191=VECTOR('',#20959,10.);
#7938=VERTEX_POINT('',#41784);
#7939=VERTEX_POINT('',#41785);
#7940=VERTEX_POINT('',#41790);
#7941=VERTEX_POINT('',#41808);
#7942=VERTEX_POINT('',#41831);
#7943=VERTEX_POINT('',#41833);
#7944=VERTEX_POINT('',#41838);
#7945=VERTEX_POINT('',#41840);
#7946=VERTEX_POINT('',#41847);
#7947=VERTEX_POINT('',#41849);
#7948=VERTEX_POINT('',#42587);
#7949=VERTEX_POINT('',#42674);
#7950=VERTEX_POINT('',#42840);
#7951=VERTEX_POINT('',#42841);
#7952=VERTEX_POINT('',#43613);
#7953=VERTEX_POINT('',#43700);
#10045=EDGE_CURVE('',#7938,#7939,#4080,.T.);
#10046=EDGE_CURVE('',#7939,#7940,#4081,.T.);
#10047=EDGE_CURVE('',#7940,#7941,#4082,.T.);
#10048=EDGE_CURVE('',#7941,#7938,#4083,.T.);
#10049=EDGE_CURVE('',#7942,#7938,#4772,.T.);
#10050=EDGE_CURVE('',#7943,#7942,#4084,.T.);
#10051=EDGE_CURVE('',#7943,#7944,#4773,.T.);
#10052=EDGE_CURVE('',#7945,#7944,#4085,.T.);
#10053=EDGE_CURVE('',#7945,#7946,#4774,.T.);
#10054=EDGE_CURVE('',#7947,#7946,#4086,.T.);
#10055=EDGE_CURVE('',#7939,#7947,#4775,.T.);
#10056=EDGE_CURVE('',#7948,#7941,#4776,.T.);
#10057=EDGE_CURVE('',#7942,#7948,#4087,.T.);
#10058=EDGE_CURVE('',#7948,#7949,#4088,.T.);
#10059=EDGE_CURVE('',#7949,#7943,#4089,.T.);
#10060=EDGE_CURVE('',#7950,#7951,#4090,.T.);
#10061=EDGE_CURVE('',#7951,#7947,#4091,.T.);
#10062=EDGE_CURVE('',#7946,#7950,#4092,.T.);
#10063=EDGE_CURVE('',#7952,#7945,#4093,.T.);
#10064=EDGE_CURVE('',#7952,#7950,#4777,.T.);
#10065=EDGE_CURVE('',#7953,#7952,#4094,.T.);
#10066=EDGE_CURVE('',#7944,#7953,#4095,.T.);
#10067=EDGE_CURVE('',#7951,#7940,#4778,.T.);
#10068=EDGE_CURVE('',#7953,#7949,#4779,.T.);
#13675=ORIENTED_EDGE('',*,*,#10045,.T.);
#13676=ORIENTED_EDGE('',*,*,#10046,.T.);
#13677=ORIENTED_EDGE('',*,*,#10047,.T.);
#13678=ORIENTED_EDGE('',*,*,#10048,.T.);
#13679=ORIENTED_EDGE('',*,*,#10045,.F.);
#13680=ORIENTED_EDGE('',*,*,#10049,.F.);
#13681=ORIENTED_EDGE('',*,*,#10050,.F.);
#13682=ORIENTED_EDGE('',*,*,#10051,.T.);
#13683=ORIENTED_EDGE('',*,*,#10052,.F.);
#13684=ORIENTED_EDGE('',*,*,#10053,.T.);
#13685=ORIENTED_EDGE('',*,*,#10054,.F.);
#13686=ORIENTED_EDGE('',*,*,#10055,.F.);
#13687=ORIENTED_EDGE('',*,*,#10048,.F.);
#13688=ORIENTED_EDGE('',*,*,#10056,.F.);
#13689=ORIENTED_EDGE('',*,*,#10057,.F.);
#13690=ORIENTED_EDGE('',*,*,#10049,.T.);
#13691=ORIENTED_EDGE('',*,*,#10050,.T.);
#13692=ORIENTED_EDGE('',*,*,#10057,.T.);
#13693=ORIENTED_EDGE('',*,*,#10058,.T.);
#13694=ORIENTED_EDGE('',*,*,#10059,.T.);
#13695=ORIENTED_EDGE('',*,*,#10060,.T.);
#13696=ORIENTED_EDGE('',*,*,#10061,.T.);
#13697=ORIENTED_EDGE('',*,*,#10054,.T.);
#13698=ORIENTED_EDGE('',*,*,#10062,.T.);
#13699=ORIENTED_EDGE('',*,*,#10062,.F.);
#13700=ORIENTED_EDGE('',*,*,#10053,.F.);
#13701=ORIENTED_EDGE('',*,*,#10063,.F.);
#13702=ORIENTED_EDGE('',*,*,#10064,.T.);
#13703=ORIENTED_EDGE('',*,*,#10065,.T.);
#13704=ORIENTED_EDGE('',*,*,#10063,.T.);
#13705=ORIENTED_EDGE('',*,*,#10052,.T.);
#13706=ORIENTED_EDGE('',*,*,#10066,.T.);
#13707=ORIENTED_EDGE('',*,*,#10047,.F.);
#13708=ORIENTED_EDGE('',*,*,#10067,.F.);
#13709=ORIENTED_EDGE('',*,*,#10060,.F.);
#13710=ORIENTED_EDGE('',*,*,#10064,.F.);
#13711=ORIENTED_EDGE('',*,*,#10065,.F.);
#13712=ORIENTED_EDGE('',*,*,#10068,.T.);
#13713=ORIENTED_EDGE('',*,*,#10058,.F.);
#13714=ORIENTED_EDGE('',*,*,#10056,.T.);
#13715=ORIENTED_EDGE('',*,*,#10046,.F.);
#13716=ORIENTED_EDGE('',*,*,#10055,.T.);
#13717=ORIENTED_EDGE('',*,*,#10061,.F.);
#13718=ORIENTED_EDGE('',*,*,#10067,.T.);
#13719=ORIENTED_EDGE('',*,*,#10059,.F.);
#13720=ORIENTED_EDGE('',*,*,#10068,.F.);
#13721=ORIENTED_EDGE('',*,*,#10066,.F.);
#13722=ORIENTED_EDGE('',*,*,#10051,.F.);
#17660=ADVANCED_FACE('',(#1632),#123,.T.);
#17661=ADVANCED_FACE('',(#1633),#397,.T.);
#17662=ADVANCED_FACE('',(#1634),#1078,.T.);
#17663=ADVANCED_FACE('',(#1635),#124,.T.);
#17664=ADVANCED_FACE('',(#1636),#125,.T.);
#17665=ADVANCED_FACE('',(#1637),#1079,.T.);
#17666=ADVANCED_FACE('',(#1638),#126,.T.);
#17667=ADVANCED_FACE('',(#1639),#398,.T.);
#17668=ADVANCED_FACE('',(#1640),#399,.T.);
#17669=ADVANCED_FACE('',(#1641),#400,.F.);
#18298=CLOSED_SHELL('',(#17660,#17661,#17662,#17663,#17664,#17665,#17666,
#17667,#17668,#17669));
#18916=AXIS2_PLACEMENT_3D('',#41715,#20946,#20947);
#18917=AXIS2_PLACEMENT_3D('',#41830,#20948,#20949);
#18918=AXIS2_PLACEMENT_3D('',#43722,#20956,#20957);
#18919=AXIS2_PLACEMENT_3D('',#43725,#20960,#20961);
#18920=AXIS2_PLACEMENT_3D('',#43726,#20962,#20963);
#20946=DIRECTION('axis',(0.,0.,1.));
#20947=DIRECTION('refdir',(1.,0.,0.));
#20948=DIRECTION('center_axis',(0.,0.0210510764790368,0.999778401536597));
#20949=DIRECTION('ref_axis',(0.,-0.999778401536597,0.0210510764790368));
#20950=DIRECTION('',(1.,0.,0.));
#20951=DIRECTION('',(0.,-0.999778401536597,0.0210510764790368));
#20952=DIRECTION('',(1.,0.,0.));
#20953=DIRECTION('',(0.,-0.999778401536597,0.0210510764790368));
#20954=DIRECTION('',(1.,0.,0.));
#20955=DIRECTION('',(1.,0.,0.));
#20956=DIRECTION('center_axis',(0.,0.0210510764790365,-0.999778401536597));
#20957=DIRECTION('ref_axis',(0.,0.999778401536597,0.0210510764790365));
#20958=DIRECTION('',(0.,0.999778401536597,0.0210510764790365));
#20959=DIRECTION('',(0.,0.999778401536597,0.0210510764790365));
#20960=DIRECTION('center_axis',(1.,0.,0.));
#20961=DIRECTION('ref_axis',(0.,0.,-1.));
#20962=DIRECTION('center_axis',(1.,0.,0.));
#20963=DIRECTION('ref_axis',(0.,0.,-1.));
#41715=CARTESIAN_POINT('',(0.,0.,0.));
#41716=CARTESIAN_POINT('Ctrl Pts',(1.5,9.34792819335158,0.196820971183211));
#41717=CARTESIAN_POINT('Ctrl Pts',(1.5,9.31857873039711,1.58780851273504));
#41718=CARTESIAN_POINT('Ctrl Pts',(1.5,8.63089363219759,4.34947211834324));
#41719=CARTESIAN_POINT('Ctrl Pts',(1.5,5.91232099870426,7.64758018279904));
#41720=CARTESIAN_POINT('Ctrl Pts',(1.5,2.03684458018563,9.44764359291464));
#41721=CARTESIAN_POINT('Ctrl Pts',(1.5,-2.23465367101115,9.40328083925727));
#41722=CARTESIAN_POINT('Ctrl Pts',(1.5,-6.07247560093714,7.5197369392284));
#41723=CARTESIAN_POINT('Ctrl Pts',(1.5,-8.42352750439441,4.54058319300765));
#41724=CARTESIAN_POINT('Ctrl Pts',(1.5,-9.66239336793898,0.50765700696431));
#41725=CARTESIAN_POINT('Ctrl Pts',(1.5,-9.0914057647348,-3.31385015859821));
#41726=CARTESIAN_POINT('Ctrl Pts',(1.5,-6.46482759358799,-7.19978040884221));
#41727=CARTESIAN_POINT('Ctrl Pts',(1.5,-2.7147574693153,-9.40315161601262));
#41728=CARTESIAN_POINT('Ctrl Pts',(1.5,2.03893109606151,-9.44584841818117));
#41729=CARTESIAN_POINT('Ctrl Pts',(1.5,5.91067968856048,-7.64792860715505));
#41730=CARTESIAN_POINT('Ctrl Pts',(1.5,8.63155746153459,-4.34908545280644));
#41731=CARTESIAN_POINT('Ctrl Pts',(1.5,9.3185787303843,-1.58780851274609));
#41732=CARTESIAN_POINT('Ctrl Pts',(1.5,9.34792819335161,-0.196820971181858));
#41733=CARTESIAN_POINT('Ctrl Pts',(1.45,9.39791706710028,0.197875722972423));
#41734=CARTESIAN_POINT('Ctrl Pts',(1.45,9.36841130719358,1.59627079745483));
#41735=CARTESIAN_POINT('Ctrl Pts',(1.45000000000001,8.67704692960724,4.37273923776376));
#41736=CARTESIAN_POINT('Ctrl Pts',(1.45,5.94393811041667,7.68847040785079));
#41737=CARTESIAN_POINT('Ctrl Pts',(1.45,2.0477365935102,9.49816718220173));
#41738=CARTESIAN_POINT('Ctrl Pts',(1.45,-2.24660356695236,9.45356424486553));
#41739=CARTESIAN_POINT('Ctrl Pts',(1.45,-6.10494877909688,7.55994984692236));
#41740=CARTESIAN_POINT('Ctrl Pts',(1.45,-8.46857308722318,4.56486422226556));
#41741=CARTESIAN_POINT('Ctrl Pts',(1.45,-9.71406393286648,0.510371735787382));
#41742=CARTESIAN_POINT('Ctrl Pts',(1.45,-9.14002288270658,-3.33157108555998));
#41743=CARTESIAN_POINT('Ctrl Pts',(1.45,-6.49939890496966,-7.2382822672017));
#41744=CARTESIAN_POINT('Ctrl Pts',(1.45,-2.72927477425517,-9.45343444662248));
#41745=CARTESIAN_POINT('Ctrl Pts',(1.45,2.04983424399026,-9.49636284253881));
#41746=CARTESIAN_POINT('Ctrl Pts',(1.45,5.94228810749773,-7.6888194897843));
#41747=CARTESIAN_POINT('Ctrl Pts',(1.45,8.67771429107584,-4.37235077790246));
#41748=CARTESIAN_POINT('Ctrl Pts',(1.45,9.36841130718074,-1.59627079746426));
#41749=CARTESIAN_POINT('Ctrl Pts',(1.45,9.3979170671003,-0.197875722971522));
#41750=CARTESIAN_POINT('Ctrl Pts',(1.4,9.44790594084898,0.198930474761635));
#41751=CARTESIAN_POINT('Ctrl Pts',(1.4,9.41824388399005,1.60473308217462));
#41752=CARTESIAN_POINT('Ctrl Pts',(1.40000000000001,8.72320022701689,4.39600635718428));
#41753=CARTESIAN_POINT('Ctrl Pts',(1.4,5.97555522212907,7.72936063290253));
#41754=CARTESIAN_POINT('Ctrl Pts',(1.4,2.05862860683477,9.54869077148881));
#41755=CARTESIAN_POINT('Ctrl Pts',(1.4,-2.25855346289357,9.50384765047379));
#41756=CARTESIAN_POINT('Ctrl Pts',(1.4,-6.13742195725662,7.60016275461633));
#41757=CARTESIAN_POINT('Ctrl Pts',(1.4,-8.51361867005195,4.58914525152347));
#41758=CARTESIAN_POINT('Ctrl Pts',(1.4,-9.76573449779398,0.513086464610454));
#41759=CARTESIAN_POINT('Ctrl Pts',(1.4,-9.18864000067837,-3.34929201252174));
#41760=CARTESIAN_POINT('Ctrl Pts',(1.4,-6.53397021635133,-7.27678412556119));
#41761=CARTESIAN_POINT('Ctrl Pts',(1.4,-2.74379207919505,-9.50371727723233));
#41762=CARTESIAN_POINT('Ctrl Pts',(1.4,2.06073739191902,-9.54687726689644));
#41763=CARTESIAN_POINT('Ctrl Pts',(1.4,5.97389652643498,-7.72971037241354));
#41764=CARTESIAN_POINT('Ctrl Pts',(1.4,8.72387112061707,-4.39561610299849));
#41765=CARTESIAN_POINT('Ctrl Pts',(1.4,9.41824388397717,-1.60473308218242));
#41766=CARTESIAN_POINT('Ctrl Pts',(1.4,9.44790594084899,-0.198930474761186));
#41767=CARTESIAN_POINT('Ctrl Pts',(1.35,9.49789481459768,0.199985226550847));
#41768=CARTESIAN_POINT('Ctrl Pts',(1.35,9.46807646078652,1.61319536689441));
#41769=CARTESIAN_POINT('Ctrl Pts',(1.35000000000002,8.76935352442654,4.4192734766048));
#41770=CARTESIAN_POINT('Ctrl Pts',(1.35,6.00717233384148,7.77025085795428));
#41771=CARTESIAN_POINT('Ctrl Pts',(1.35,2.06952062015934,9.59921436077589));
#41772=CARTESIAN_POINT('Ctrl Pts',(1.35,-2.27050335883478,9.55413105608205));
#41773=CARTESIAN_POINT('Ctrl Pts',(1.35,-6.16989513541637,7.64037566231029));
#41774=CARTESIAN_POINT('Ctrl Pts',(1.35,-8.55866425288072,4.61342628078139));
#41775=CARTESIAN_POINT('Ctrl Pts',(1.35,-9.81740506272147,0.515801193433526));
#41776=CARTESIAN_POINT('Ctrl Pts',(1.35,-9.23725711865016,-3.3670129394835));
#41777=CARTESIAN_POINT('Ctrl Pts',(1.35,-6.568541527733,-7.31528598392068));
#41778=CARTESIAN_POINT('Ctrl Pts',(1.35,-2.75830938413493,-9.55400010784217));
#41779=CARTESIAN_POINT('Ctrl Pts',(1.35,2.07164053984778,-9.59739169125409));
#41780=CARTESIAN_POINT('Ctrl Pts',(1.35,6.00550494537223,-7.77060125504278));
#41781=CARTESIAN_POINT('Ctrl Pts',(1.35,8.77002795015831,-4.41888142809452));
#41782=CARTESIAN_POINT('Ctrl Pts',(1.35,9.46807646077361,-1.61319536690059));
#41783=CARTESIAN_POINT('Ctrl Pts',(1.35,9.49789481459768,-0.19998522655085));
#41784=CARTESIAN_POINT('',(1.35,9.49789481459768,-0.19998522655085));
#41785=CARTESIAN_POINT('',(1.5,9.3479280542199,-0.196827565075829));
#41786=CARTESIAN_POINT('Ctrl Pts',(1.35,9.49789481459768,-0.19998522655085));
#41787=CARTESIAN_POINT('Ctrl Pts',(1.4,9.44790594084899,-0.198930474761186));
#41788=CARTESIAN_POINT('Ctrl Pts',(1.45,9.3979170671003,-0.197875722971522));
#41789=CARTESIAN_POINT('Ctrl Pts',(1.5,9.34792819335161,-0.196820971181858));
#41790=CARTESIAN_POINT('',(1.5,9.3479280542199,0.196827565075824));
#41791=CARTESIAN_POINT('Ctrl Pts',(1.5,9.34792805421988,-0.196827565075189));
#41792=CARTESIAN_POINT('Ctrl Pts',(1.5,9.31857764478916,-1.58781287596857));
#41793=CARTESIAN_POINT('Ctrl Pts',(1.5,8.63155602840585,-4.34908719035855));
#41794=CARTESIAN_POINT('Ctrl Pts',(1.5,5.91067968856048,-7.64792860715505));
#41795=CARTESIAN_POINT('Ctrl Pts',(1.5,2.03893109606151,-9.44584841818117));
#41796=CARTESIAN_POINT('Ctrl Pts',(1.5,-2.7147574693153,-9.40315161601262));
#41797=CARTESIAN_POINT('Ctrl Pts',(1.5,-6.46482759358799,-7.19978040884221));
#41798=CARTESIAN_POINT('Ctrl Pts',(1.5,-9.0914057647348,-3.31385015859821));
#41799=CARTESIAN_POINT('Ctrl Pts',(1.5,-9.66239336793898,0.50765700696431));
#41800=CARTESIAN_POINT('Ctrl Pts',(1.5,-8.42352750439441,4.54058319300765));
#41801=CARTESIAN_POINT('Ctrl Pts',(1.5,-6.07247560093714,7.5197369392284));
#41802=CARTESIAN_POINT('Ctrl Pts',(1.5,-2.23465367101115,9.40328083925727));
#41803=CARTESIAN_POINT('Ctrl Pts',(1.5,2.03684458018563,9.44764359291464));
#41804=CARTESIAN_POINT('Ctrl Pts',(1.5,5.91232099870426,7.64758018279904));
#41805=CARTESIAN_POINT('Ctrl Pts',(1.5,8.63089076836887,4.34947559267255));
#41806=CARTESIAN_POINT('Ctrl Pts',(1.5,9.31857655710787,1.58781724039989));
#41807=CARTESIAN_POINT('Ctrl Pts',(1.5,9.34792791508345,0.196834158967628));
#41808=CARTESIAN_POINT('',(1.35,9.49789481459768,0.199985226550847));
#41809=CARTESIAN_POINT('Ctrl Pts',(1.5,9.34792805421986,0.196827565076001));
#41810=CARTESIAN_POINT('Ctrl Pts',(1.45,9.39791692722763,0.197882351980178));
#41811=CARTESIAN_POINT('Ctrl Pts',(1.4,9.4479058002354,0.198937138884354));
#41812=CARTESIAN_POINT('Ctrl Pts',(1.35,9.49789467324317,0.199991925788531));
#41813=CARTESIAN_POINT('Ctrl Pts',(1.35,9.49789481459768,0.199985226550847));
#41814=CARTESIAN_POINT('Ctrl Pts',(1.35,9.46807646078652,1.61319536689441));
#41815=CARTESIAN_POINT('Ctrl Pts',(1.35000000000002,8.76935352442654,4.4192734766048));
#41816=CARTESIAN_POINT('Ctrl Pts',(1.35,6.00717233384148,7.77025085795428));
#41817=CARTESIAN_POINT('Ctrl Pts',(1.35,2.06952062015934,9.59921436077589));
#41818=CARTESIAN_POINT('Ctrl Pts',(1.35,-2.27050335883478,9.55413105608205));
#41819=CARTESIAN_POINT('Ctrl Pts',(1.35,-6.16989513541637,7.64037566231029));
#41820=CARTESIAN_POINT('Ctrl Pts',(1.35,-8.55866425288072,4.61342628078139));
#41821=CARTESIAN_POINT('Ctrl Pts',(1.35,-9.81740506272147,0.515801193433526));
#41822=CARTESIAN_POINT('Ctrl Pts',(1.35,-9.23725711865016,-3.3670129394835));
#41823=CARTESIAN_POINT('Ctrl Pts',(1.35,-6.568541527733,-7.31528598392068));
#41824=CARTESIAN_POINT('Ctrl Pts',(1.35,-2.75830938413493,-9.55400010784217));
#41825=CARTESIAN_POINT('Ctrl Pts',(1.35,2.07164053984778,-9.59739169125409));
#41826=CARTESIAN_POINT('Ctrl Pts',(1.35,6.00550494537223,-7.77060125504278));
#41827=CARTESIAN_POINT('Ctrl Pts',(1.35,8.77002795015831,-4.41888142809452));
#41828=CARTESIAN_POINT('Ctrl Pts',(1.35,9.46807646077361,-1.61319536690059));
#41829=CARTESIAN_POINT('Ctrl Pts',(1.35,9.49789481459768,-0.19998522655085));
#41830=CARTESIAN_POINT('Origin',(0.,9.49789481459768,-0.19998522655085));
#41831=CARTESIAN_POINT('',(0.15,9.49789474391925,-0.1999885761703));
#41832=CARTESIAN_POINT('',(0.,9.49789481459768,-0.19998522655085));
#41833=CARTESIAN_POINT('',(0.,9.3479280542199,-0.196827565075894));
#41834=CARTESIAN_POINT('Ctrl Pts',(0.,9.3479280542199,-0.196827565075896));
#41835=CARTESIAN_POINT('Ctrl Pts',(0.05,9.39791692722766,-0.197882351980531));
#41836=CARTESIAN_POINT('Ctrl Pts',(0.1,9.44790580023542,-0.198937138885166));
#41837=CARTESIAN_POINT('Ctrl Pts',(0.15,9.49789467324318,-0.199991925789801));
#41838=CARTESIAN_POINT('',(0.,8.14819397266823,-0.171566273307202));
#41839=CARTESIAN_POINT('',(0.,9.49789481459768,-0.19998522655085));
#41840=CARTESIAN_POINT('',(0.15,7.99822721229277,-0.168408611832295));
#41841=CARTESIAN_POINT('Ctrl Pts',(0.15,7.99822721229278,-0.168408611832294));
#41842=CARTESIAN_POINT('Ctrl Pts',(0.125000000000001,8.02322167235535,-0.168934888744779));
#41843=CARTESIAN_POINT('Ctrl Pts',(0.1,8.04821613241793,-0.169461165657263));
#41844=CARTESIAN_POINT('Ctrl Pts',(0.0500000000000007,8.09820505254308,
-0.170513719482233));
#41845=CARTESIAN_POINT('Ctrl Pts',(0.0250000000000003,8.12319951260566,
-0.171039996394718));
#41846=CARTESIAN_POINT('Ctrl Pts',(0.,8.14819397266823,-0.171566273307203));
#41847=CARTESIAN_POINT('',(1.35,7.99822721229278,-0.168408611832294));
#41848=CARTESIAN_POINT('',(0.,7.99822721229278,-0.168408611832294));
#41849=CARTESIAN_POINT('',(1.5,8.14819397266823,-0.171566273307202));
#41850=CARTESIAN_POINT('Ctrl Pts',(1.5,8.14819397266823,-0.171566273307202));
#41851=CARTESIAN_POINT('Ctrl Pts',(1.475,8.12319951260566,-0.171039996394717));
#41852=CARTESIAN_POINT('Ctrl Pts',(1.45,8.09820505254308,-0.170513719482232));
#41853=CARTESIAN_POINT('Ctrl Pts',(1.4,8.04821613241793,-0.169461165657263));
#41854=CARTESIAN_POINT('Ctrl Pts',(1.375,8.02322167235535,-0.168934888744779));
#41855=CARTESIAN_POINT('Ctrl Pts',(1.35,7.99822721229278,-0.168408611832294));
#41856=CARTESIAN_POINT('',(1.5,9.49789481459768,-0.19998522655085));
#41857=CARTESIAN_POINT('Ctrl Pts',(0.,9.49789481459768,0.199985226550847));
#41858=CARTESIAN_POINT('Ctrl Pts',(1.5,9.49789481459768,0.199985226550847));
#41859=CARTESIAN_POINT('Ctrl Pts',(0.,9.49719905300875,0.23296012982553));
#41860=CARTESIAN_POINT('Ctrl Pts',(1.5,9.49719905300875,0.23296012982553));
#41861=CARTESIAN_POINT('Ctrl Pts',(0.,9.49552283633777,0.298887663038565));
#41862=CARTESIAN_POINT('Ctrl Pts',(1.5,9.49552283633777,0.298887663038565));
#41863=CARTESIAN_POINT('Ctrl Pts',(0.,9.49215443085195,0.397712142849129));
#41864=CARTESIAN_POINT('Ctrl Pts',(1.5,9.49215443085195,0.397712142849129));
#41865=CARTESIAN_POINT('Ctrl Pts',(0.,9.48595504112623,0.529344474233868));
#41866=CARTESIAN_POINT('Ctrl Pts',(1.5,9.48595504112623,0.529344474233868));
#41867=CARTESIAN_POINT('Ctrl Pts',(0.,9.47535906724825,0.693659210071412));
#41868=CARTESIAN_POINT('Ctrl Pts',(1.5,9.47535906724825,0.693659210071412));
#41869=CARTESIAN_POINT('Ctrl Pts',(0.,9.46191727310055,0.857739457490273));
#41870=CARTESIAN_POINT('Ctrl Pts',(1.5,9.46191727310055,0.857739457490273));
#41871=CARTESIAN_POINT('Ctrl Pts',(0.,9.44563165255892,1.02156760869831));
#41872=CARTESIAN_POINT('Ctrl Pts',(1.5,9.44563165255892,1.02156760869831));
#41873=CARTESIAN_POINT('Ctrl Pts',(0.,9.42650567192302,1.18511432783379));
#41874=CARTESIAN_POINT('Ctrl Pts',(1.5,9.42650567192302,1.18511432783379));
#41875=CARTESIAN_POINT('Ctrl Pts',(0.,9.40454466499295,1.34833562021875));
#41876=CARTESIAN_POINT('Ctrl Pts',(1.5,9.40454466499295,1.34833562021875));
#41877=CARTESIAN_POINT('Ctrl Pts',(0.,9.37975553550412,1.51117719524862));
#41878=CARTESIAN_POINT('Ctrl Pts',(1.5,9.37975553550412,1.51117719524862));
#41879=CARTESIAN_POINT('Ctrl Pts',(0.,9.3521464596427,1.67357882889248));
#41880=CARTESIAN_POINT('Ctrl Pts',(1.5,9.3521464596427,1.67357882889248));
#41881=CARTESIAN_POINT('Ctrl Pts',(0.,9.32172658862998,1.83547872597431));
#41882=CARTESIAN_POINT('Ctrl Pts',(1.5,9.32172658862998,1.83547872597431));
#41883=CARTESIAN_POINT('Ctrl Pts',(0.,9.28850575136458,1.99681788239688));
#41884=CARTESIAN_POINT('Ctrl Pts',(1.5,9.28850575136458,1.99681788239688));
#41885=CARTESIAN_POINT('Ctrl Pts',(0.,9.25249415711072,2.15754444747772));
#41886=CARTESIAN_POINT('Ctrl Pts',(1.5,9.25249415711072,2.15754444747772));
#41887=CARTESIAN_POINT('Ctrl Pts',(0.,9.21370252437557,2.31761173346451));
#41888=CARTESIAN_POINT('Ctrl Pts',(1.5,9.21370252437557,2.31761173346451));
#41889=CARTESIAN_POINT('Ctrl Pts',(0.,9.17214220982581,2.47697622525282));
#41890=CARTESIAN_POINT('Ctrl Pts',(1.5,9.17214220982581,2.47697622525282));
#41891=CARTESIAN_POINT('Ctrl Pts',(0.,9.12782533724969,2.63559559022678));
#41892=CARTESIAN_POINT('Ctrl Pts',(1.5,9.12782533724969,2.63559559022678));
#41893=CARTESIAN_POINT('Ctrl Pts',(0.,9.08076492656775,2.7934266881506));
#41894=CARTESIAN_POINT('Ctrl Pts',(1.5,9.08076492656775,2.7934266881506));
#41895=CARTESIAN_POINT('Ctrl Pts',(0.,9.03097502289868,2.95042358103354));
#41896=CARTESIAN_POINT('Ctrl Pts',(1.5,9.03097502289868,2.95042358103354));
#41897=CARTESIAN_POINT('Ctrl Pts',(0.,8.97847063443715,3.10653841617385));
#41898=CARTESIAN_POINT('Ctrl Pts',(1.5,8.97847063443715,3.10653841617385));
#41899=CARTESIAN_POINT('Ctrl Pts',(0.,8.92326767038838,3.26172230913519));
#41900=CARTESIAN_POINT('Ctrl Pts',(1.5,8.92326767038838,3.26172230913519));
#41901=CARTESIAN_POINT('Ctrl Pts',(0.,8.86538287895681,3.41592622669136));
#41902=CARTESIAN_POINT('Ctrl Pts',(1.5,8.86538287895681,3.41592622669136));
#41903=CARTESIAN_POINT('Ctrl Pts',(0.,8.80483378538669,3.56910186977197));
#41904=CARTESIAN_POINT('Ctrl Pts',(1.5,8.80483378538669,3.56910186977197));
#41905=CARTESIAN_POINT('Ctrl Pts',(0.,8.74163863005133,3.7212025564438));
#41906=CARTESIAN_POINT('Ctrl Pts',(1.5,8.74163863005133,3.7212025564438));
#41907=CARTESIAN_POINT('Ctrl Pts',(0.,8.67581638707764,3.8721828611177));
#41908=CARTESIAN_POINT('Ctrl Pts',(1.5,8.67581638707764,3.8721828611177));
#41909=CARTESIAN_POINT('Ctrl Pts',(0.,8.60738678301798,4.02199825381135));
#41910=CARTESIAN_POINT('Ctrl Pts',(1.5,8.60738678301798,4.02199825381135));
#41911=CARTESIAN_POINT('Ctrl Pts',(0.,8.53637031556992,4.17060473945411));
#41912=CARTESIAN_POINT('Ctrl Pts',(1.5,8.53637031556992,4.17060473945411));
#41913=CARTESIAN_POINT('Ctrl Pts',(0.,8.46278827234408,4.31795849722051));
#41914=CARTESIAN_POINT('Ctrl Pts',(1.5,8.46278827234408,4.31795849722051));
#41915=CARTESIAN_POINT('Ctrl Pts',(0.,8.38666274968139,4.46401551987939));
#41916=CARTESIAN_POINT('Ctrl Pts',(1.5,8.38666274968139,4.46401551987939));
#41917=CARTESIAN_POINT('Ctrl Pts',(0.,8.30801663482879,4.60873178803206));
#41918=CARTESIAN_POINT('Ctrl Pts',(1.5,8.30801663482879,4.60873178803206));
#41919=CARTESIAN_POINT('Ctrl Pts',(0.,8.22687358816372,4.75206344435896));
#41920=CARTESIAN_POINT('Ctrl Pts',(1.5,8.22687358816372,4.75206344435896));
#41921=CARTESIAN_POINT('Ctrl Pts',(0.,8.14325802546687,4.89396696788329));
#41922=CARTESIAN_POINT('Ctrl Pts',(1.5,8.14325802546687,4.89396696788329));
#41923=CARTESIAN_POINT('Ctrl Pts',(0.,8.05719510024166,5.03439934825727));
#41924=CARTESIAN_POINT('Ctrl Pts',(1.5,8.05719510024166,5.03439934825727));
#41925=CARTESIAN_POINT('Ctrl Pts',(0.,7.96871068608006,5.17331826007837));
#41926=CARTESIAN_POINT('Ctrl Pts',(1.5,7.96871068608006,5.17331826007837));
#41927=CARTESIAN_POINT('Ctrl Pts',(0.,7.87783137293423,5.31068200583127));
#41928=CARTESIAN_POINT('Ctrl Pts',(1.5,7.87783137293423,5.31068200583127));
#41929=CARTESIAN_POINT('Ctrl Pts',(0.,7.78458446343339,5.44644945886476));
#41930=CARTESIAN_POINT('Ctrl Pts',(1.5,7.78458446343339,5.44644945886476));
#41931=CARTESIAN_POINT('Ctrl Pts',(0.,7.68899796924526,5.58058000640172));
#41932=CARTESIAN_POINT('Ctrl Pts',(1.5,7.68899796924526,5.58058000640172));
#41933=CARTESIAN_POINT('Ctrl Pts',(0.,7.59110060748197,5.7130334925803));
#41934=CARTESIAN_POINT('Ctrl Pts',(1.5,7.59110060748197,5.7130334925803));
#41935=CARTESIAN_POINT('Ctrl Pts',(0.,7.49092179714982,5.84377016152442));
#41936=CARTESIAN_POINT('Ctrl Pts',(1.5,7.49092179714982,5.84377016152442));
#41937=CARTESIAN_POINT('Ctrl Pts',(0.,7.38849164783963,5.97275069881958));
#41938=CARTESIAN_POINT('Ctrl Pts',(1.5,7.38849164783963,5.97275069881958));
#41939=CARTESIAN_POINT('Ctrl Pts',(0.,7.28384094846006,6.09993627301787));
#41940=CARTESIAN_POINT('Ctrl Pts',(1.5,7.28384094846006,6.09993627301787));
#41941=CARTESIAN_POINT('Ctrl Pts',(0.,7.17700115601342,6.22528857717439));
#41942=CARTESIAN_POINT('Ctrl Pts',(1.5,7.17700115601342,6.22528857717439));
#41943=CARTESIAN_POINT('Ctrl Pts',(0.,7.06800438441268,6.34876987041675));
#41944=CARTESIAN_POINT('Ctrl Pts',(1.5,7.06800438441268,6.34876987041675));
#41945=CARTESIAN_POINT('Ctrl Pts',(0.,6.95688339333978,6.47034301954938));
#41946=CARTESIAN_POINT('Ctrl Pts',(1.5,6.95688339333978,6.47034301954938));
#41947=CARTESIAN_POINT('Ctrl Pts',(0.,6.84367157878497,6.58997149692307));
#41948=CARTESIAN_POINT('Ctrl Pts',(1.5,6.84367157878497,6.58997149692307));
#41949=CARTESIAN_POINT('Ctrl Pts',(0.,6.72840296362591,6.70761937834073));
#41950=CARTESIAN_POINT('Ctrl Pts',(1.5,6.72840296362591,6.70761937834073));
#41951=CARTESIAN_POINT('Ctrl Pts',(0.,6.61111218824589,6.82325134100059));
#41952=CARTESIAN_POINT('Ctrl Pts',(1.5,6.61111218824589,6.82325134100059));
#41953=CARTESIAN_POINT('Ctrl Pts',(0.,6.4918345011908,6.93683266147689));
#41954=CARTESIAN_POINT('Ctrl Pts',(1.5,6.4918345011908,6.93683266147689));
#41955=CARTESIAN_POINT('Ctrl Pts',(0.,6.37060574986377,7.04832921373777));
#41956=CARTESIAN_POINT('Ctrl Pts',(1.5,6.37060574986377,7.04832921373777));
#41957=CARTESIAN_POINT('Ctrl Pts',(0.,6.24746236896056,7.15770748449017));
#41958=CARTESIAN_POINT('Ctrl Pts',(1.5,6.24746236896056,7.15770748449017));
#41959=CARTESIAN_POINT('Ctrl Pts',(0.,6.12244136894179,7.26493458856336));
#41960=CARTESIAN_POINT('Ctrl Pts',(1.5,6.12244136894179,7.26493458856336));
#41961=CARTESIAN_POINT('Ctrl Pts',(0.,5.99558032454086,7.3699782843317));
#41962=CARTESIAN_POINT('Ctrl Pts',(1.5,5.99558032454086,7.3699782843317));
#41963=CARTESIAN_POINT('Ctrl Pts',(0.,5.86691736330732,7.47280698917791));
#41964=CARTESIAN_POINT('Ctrl Pts',(1.5,5.86691736330732,7.47280698917791));
#41965=CARTESIAN_POINT('Ctrl Pts',(0.,5.73649115418445,7.57338979499723));
#41966=CARTESIAN_POINT('Ctrl Pts',(1.5,5.73649115418445,7.57338979499723));
#41967=CARTESIAN_POINT('Ctrl Pts',(0.,5.60434089566038,7.67169647460986));
#41968=CARTESIAN_POINT('Ctrl Pts',(1.5,5.60434089566038,7.67169647460986));
#41969=CARTESIAN_POINT('Ctrl Pts',(0.,5.47050630395207,7.76769748821551));
#41970=CARTESIAN_POINT('Ctrl Pts',(1.5,5.47050630395207,7.76769748821551));
#41971=CARTESIAN_POINT('Ctrl Pts',(0.,5.33502760122167,7.86136398989113));
#41972=CARTESIAN_POINT('Ctrl Pts',(1.5,5.33502760122167,7.86136398989113));
#41973=CARTESIAN_POINT('Ctrl Pts',(0.,5.1979455038246,7.95266783413171));
#41974=CARTESIAN_POINT('Ctrl Pts',(1.5,5.1979455038246,7.95266783413171));
#41975=CARTESIAN_POINT('Ctrl Pts',(0.,5.0593012105884,8.04158158243497));
#41976=CARTESIAN_POINT('Ctrl Pts',(1.5,5.0593012105884,8.04158158243497));
#41977=CARTESIAN_POINT('Ctrl Pts',(0.,4.9191363900222,8.12807851205385));
#41978=CARTESIAN_POINT('Ctrl Pts',(1.5,4.9191363900222,8.12807851205385));
#41979=CARTESIAN_POINT('Ctrl Pts',(0.,4.77749316755553,8.21213262479377));
#41980=CARTESIAN_POINT('Ctrl Pts',(1.5,4.77749316755553,8.21213262479377));
#41981=CARTESIAN_POINT('Ctrl Pts',(0.,4.63441411280564,8.29371865585536));
#41982=CARTESIAN_POINT('Ctrl Pts',(1.5,4.63441411280564,8.29371865585536));
#41983=CARTESIAN_POINT('Ctrl Pts',(0.,4.48994222687257,8.37281208272277));
#41984=CARTESIAN_POINT('Ctrl Pts',(1.5,4.48994222687257,8.37281208272277));
#41985=CARTESIAN_POINT('Ctrl Pts',(0.,4.34412092966134,8.44938913409869));
#41986=CARTESIAN_POINT('Ctrl Pts',(1.5,4.34412092966134,8.44938913409869));
#41987=CARTESIAN_POINT('Ctrl Pts',(0.,4.19699404656719,8.52342679605714));
#41988=CARTESIAN_POINT('Ctrl Pts',(1.5,4.19699404656719,8.52342679605714));
#41989=CARTESIAN_POINT('Ctrl Pts',(0.,4.04860579518617,8.59490281824345));
#41990=CARTESIAN_POINT('Ctrl Pts',(1.5,4.04860579518617,8.59490281824345));
#41991=CARTESIAN_POINT('Ctrl Pts',(0.,3.89900077205028,8.66379572012202));
#41992=CARTESIAN_POINT('Ctrl Pts',(1.5,3.89900077205028,8.66379572012202));
#41993=CARTESIAN_POINT('Ctrl Pts',(0.,3.74822393938623,8.73008479727191));
#41994=CARTESIAN_POINT('Ctrl Pts',(1.5,3.74822393938623,8.73008479727191));
#41995=CARTESIAN_POINT('Ctrl Pts',(0.,3.59632061189705,8.79375012773102));
#41996=CARTESIAN_POINT('Ctrl Pts',(1.5,3.59632061189705,8.79375012773102));
#41997=CARTESIAN_POINT('Ctrl Pts',(0.,3.44333644288472,8.85477257760155));
#41998=CARTESIAN_POINT('Ctrl Pts',(1.5,3.44333644288472,8.85477257760155));
#41999=CARTESIAN_POINT('Ctrl Pts',(0.,3.28931741039412,8.91313380670472));
#42000=CARTESIAN_POINT('Ctrl Pts',(1.5,3.28931741039412,8.91313380670472));
#42001=CARTESIAN_POINT('Ctrl Pts',(0.,3.13430980337712,8.96881627428495));
#42002=CARTESIAN_POINT('Ctrl Pts',(1.5,3.13430980337712,8.96881627428495));
#42003=CARTESIAN_POINT('Ctrl Pts',(0.,2.97836020787617,9.02180324476397));
#42004=CARTESIAN_POINT('Ctrl Pts',(1.5,2.97836020787617,9.02180324476397));
#42005=CARTESIAN_POINT('Ctrl Pts',(0.,2.82151549322663,9.07207879354553));
#42006=CARTESIAN_POINT('Ctrl Pts',(1.5,2.82151549322663,9.07207879354553));
#42007=CARTESIAN_POINT('Ctrl Pts',(0.,2.66382279778062,9.11962781112771));
#42008=CARTESIAN_POINT('Ctrl Pts',(1.5,2.66382279778062,9.11962781112771));
#42009=CARTESIAN_POINT('Ctrl Pts',(0.,2.50532951464783,9.16443600726607));
#42010=CARTESIAN_POINT('Ctrl Pts',(1.5,2.50532951464783,9.16443600726607));
#42011=CARTESIAN_POINT('Ctrl Pts',(0.,2.3460832774521,9.20648991518802));
#42012=CARTESIAN_POINT('Ctrl Pts',(1.5,2.3460832774521,9.20648991518802));
#42013=CARTESIAN_POINT('Ctrl Pts',(0.,2.18613194610305,9.24577689585874));
#42014=CARTESIAN_POINT('Ctrl Pts',(1.5,2.18613194610305,9.24577689585874));
#42015=CARTESIAN_POINT('Ctrl Pts',(0.,2.0255235925818,9.28228514229881));
#42016=CARTESIAN_POINT('Ctrl Pts',(1.5,2.0255235925818,9.28228514229881));
#42017=CARTESIAN_POINT('Ctrl Pts',(0.,1.86430648634783,9.31600368256167));
#42018=CARTESIAN_POINT('Ctrl Pts',(1.5,1.86430648634783,9.31600368256167));
#42019=CARTESIAN_POINT('Ctrl Pts',(0.,1.70252907975812,9.34692238276349));
#42020=CARTESIAN_POINT('Ctrl Pts',(1.5,1.70252907975812,9.34692238276349));
#42021=CARTESIAN_POINT('Ctrl Pts',(0.,1.5402399934977,9.3750319501651));
#42022=CARTESIAN_POINT('Ctrl Pts',(1.5,1.5402399934977,9.3750319501651));
#42023=CARTESIAN_POINT('Ctrl Pts',(0.,1.37748800202051,9.4003239363065));
#42024=CARTESIAN_POINT('Ctrl Pts',(1.5,1.37748800202051,9.4003239363065));
#42025=CARTESIAN_POINT('Ctrl Pts',(0.,1.21432201899992,9.42279074019417));
#42026=CARTESIAN_POINT('Ctrl Pts',(1.5,1.21432201899992,9.42279074019417));
#42027=CARTESIAN_POINT('Ctrl Pts',(0.,1.05079108253882,9.44242560995382));
#42028=CARTESIAN_POINT('Ctrl Pts',(1.5,1.05079108253882,9.44242560995382));
#42029=CARTESIAN_POINT('Ctrl Pts',(0.,0.886944340387567,9.45922264453625));
#42030=CARTESIAN_POINT('Ctrl Pts',(1.5,0.886944340387567,9.45922264453625));
#42031=CARTESIAN_POINT('Ctrl Pts',(0.,0.722831035168742,9.47317679547619));
#42032=CARTESIAN_POINT('Ctrl Pts',(1.5,0.722831035168742,9.47317679547619));
#42033=CARTESIAN_POINT('Ctrl Pts',(0.,0.558500489607787,9.48428386870474));
#42034=CARTESIAN_POINT('Ctrl Pts',(1.5,0.558500489607787,9.48428386870474));
#42035=CARTESIAN_POINT('Ctrl Pts',(0.,0.3940020917686,9.49254052641465));
#42036=CARTESIAN_POINT('Ctrl Pts',(1.5,0.3940020917686,9.49254052641465));
#42037=CARTESIAN_POINT('Ctrl Pts',(0.,0.229385280173572,9.49794428744835));
#42038=CARTESIAN_POINT('Ctrl Pts',(1.5,0.229385280173572,9.49794428744835));
#42039=CARTESIAN_POINT('Ctrl Pts',(0.,0.0646995289263127,9.5004935277393));
#42040=CARTESIAN_POINT('Ctrl Pts',(1.5,0.0646995289263127,9.5004935277393));
#42041=CARTESIAN_POINT('Ctrl Pts',(0.,-0.100005667163057,9.50018748080671));
#42042=CARTESIAN_POINT('Ctrl Pts',(1.5,-0.100005667163057,9.50018748080671));
#42043=CARTESIAN_POINT('Ctrl Pts',(0.,-0.264680807451436,9.49702623830398));
#42044=CARTESIAN_POINT('Ctrl Pts',(1.5,-0.264680807451436,9.49702623830398));
#42045=CARTESIAN_POINT('Ctrl Pts',(0.,-0.42927640033591,9.49101075062043));
#42046=CARTESIAN_POINT('Ctrl Pts',(1.5,-0.42927640033591,9.49101075062043));
#42047=CARTESIAN_POINT('Ctrl Pts',(0.,-0.593742978110499,9.48214282597012));
#42048=CARTESIAN_POINT('Ctrl Pts',(1.5,-0.593742978110499,9.48214282597012));
#42049=CARTESIAN_POINT('Ctrl Pts',(0.,-0.75803111182441,9.47042512953441));
#42050=CARTESIAN_POINT('Ctrl Pts',(1.5,-0.75803111182441,9.47042512953441));
#42051=CARTESIAN_POINT('Ctrl Pts',(0.,-0.922091426142622,9.45586118265776));
#42052=CARTESIAN_POINT('Ctrl Pts',(1.5,-0.922091426142622,9.45586118265776));
#42053=CARTESIAN_POINT('Ctrl Pts',(0.,-1.08587461420981,9.43845536209725));
#42054=CARTESIAN_POINT('Ctrl Pts',(1.5,-1.08587461420981,9.43845536209725));
#42055=CARTESIAN_POINT('Ctrl Pts',(0.,-1.24933145251863,9.41821289932518));
#42056=CARTESIAN_POINT('Ctrl Pts',(1.5,-1.24933145251863,9.41821289932518));
#42057=CARTESIAN_POINT('Ctrl Pts',(0.,-1.41241281563231,9.39513987833922));
#42058=CARTESIAN_POINT('Ctrl Pts',(1.5,-1.41241281563231,9.39513987833922));
#42059=CARTESIAN_POINT('Ctrl Pts',(0.,-1.57506969091331,9.36924323352564));
#42060=CARTESIAN_POINT('Ctrl Pts',(1.5,-1.57506969091331,9.36924323352564));
#42061=CARTESIAN_POINT('Ctrl Pts',(0.,-1.73725319325894,9.34053074757567));
#42062=CARTESIAN_POINT('Ctrl Pts',(1.5,-1.73725319325894,9.34053074757567));
#42063=CARTESIAN_POINT('Ctrl Pts',(0.,-1.89891457984514,9.30901104945495));
#42064=CARTESIAN_POINT('Ctrl Pts',(1.5,-1.89891457984514,9.30901104945495));
#42065=CARTESIAN_POINT('Ctrl Pts',(0.,-2.06000526487899,9.27469361242572));
#42066=CARTESIAN_POINT('Ctrl Pts',(1.5,-2.06000526487899,9.27469361242572));
#42067=CARTESIAN_POINT('Ctrl Pts',(0.,-2.22047683407631,9.23758875058882));
#42068=CARTESIAN_POINT('Ctrl Pts',(1.5,-2.22047683407631,9.23758875058882));
#42069=CARTESIAN_POINT('Ctrl Pts',(0.,-2.38028105914987,9.19770761547813));
#42070=CARTESIAN_POINT('Ctrl Pts',(1.5,-2.38028105914987,9.19770761547813));
#42071=CARTESIAN_POINT('Ctrl Pts',(0.,-2.53936991230918,9.15506219270728));
#42072=CARTESIAN_POINT('Ctrl Pts',(1.5,-2.53936991230918,9.15506219270728));
#42073=CARTESIAN_POINT('Ctrl Pts',(0.,-2.69769558077273,9.1096652986684));
#42074=CARTESIAN_POINT('Ctrl Pts',(1.5,-2.69769558077273,9.1096652986684));
#42075=CARTESIAN_POINT('Ctrl Pts',(0.,-2.85521048129368,9.06153057728299));
#42076=CARTESIAN_POINT('Ctrl Pts',(1.5,-2.85521048129368,9.06153057728299));
#42077=CARTESIAN_POINT('Ctrl Pts',(0.,-3.01186727428374,9.01067249530426));
#42078=CARTESIAN_POINT('Ctrl Pts',(1.5,-3.01186727428374,9.01067249530426));
#42079=CARTESIAN_POINT('Ctrl Pts',(0.,-3.16761887795222,8.95710633767099));
#42080=CARTESIAN_POINT('Ctrl Pts',(1.5,-3.16761887795222,8.95710633767099));
#42081=CARTESIAN_POINT('Ctrl Pts',(0.,-3.32241848246116,8.90084820291227));
#42082=CARTESIAN_POINT('Ctrl Pts',(1.5,-3.32241848246116,8.90084820291227));
#42083=CARTESIAN_POINT('Ctrl Pts',(0.,-3.47621956409756,8.84191499860308));
#42084=CARTESIAN_POINT('Ctrl Pts',(1.5,-3.47621956409756,8.84191499860308));
#42085=CARTESIAN_POINT('Ctrl Pts',(0.,-3.62897589946335,8.78032443687033));
#42086=CARTESIAN_POINT('Ctrl Pts',(1.5,-3.62897589946335,8.78032443687033));
#42087=CARTESIAN_POINT('Ctrl Pts',(0.,-3.78064157913952,8.71609502848983));
#42088=CARTESIAN_POINT('Ctrl Pts',(1.5,-3.78064157913952,8.71609502848983));
#42089=CARTESIAN_POINT('Ctrl Pts',(0.,-3.93117102136967,8.649246077033));
#42090=CARTESIAN_POINT('Ctrl Pts',(1.5,-3.93117102136967,8.649246077033));
#42091=CARTESIAN_POINT('Ctrl Pts',(0.,-4.08051898576423,8.57979767306322));
#42092=CARTESIAN_POINT('Ctrl Pts',(1.5,-4.08051898576423,8.57979767306322));
#42093=CARTESIAN_POINT('Ctrl Pts',(0.,-4.22864058702597,8.50777068838111));
#42094=CARTESIAN_POINT('Ctrl Pts',(1.5,-4.22864058702597,8.50777068838111));
#42095=CARTESIAN_POINT('Ctrl Pts',(0.,-4.37549130869752,8.43318677031893));
#42096=CARTESIAN_POINT('Ctrl Pts',(1.5,-4.37549130869752,8.43318677031893));
#42097=CARTESIAN_POINT('Ctrl Pts',(0.,-4.52102701626319,8.35606833467688));
#42098=CARTESIAN_POINT('Ctrl Pts',(1.5,-4.52102701626319,8.35606833467688));
#42099=CARTESIAN_POINT('Ctrl Pts',(0.,-4.66520397027454,8.27643855870735));
#42100=CARTESIAN_POINT('Ctrl Pts',(1.5,-4.66520397027454,8.27643855870735));
#42101=CARTESIAN_POINT('Ctrl Pts',(0.,-4.8079788395007,8.19432137414672));
#42102=CARTESIAN_POINT('Ctrl Pts',(1.5,-4.8079788395007,8.19432137414672));
#42103=CARTESIAN_POINT('Ctrl Pts',(0.,-4.94930871410412,8.1097414602942));
#42104=CARTESIAN_POINT('Ctrl Pts',(1.5,-4.94930871410412,8.1097414602942));
#42105=CARTESIAN_POINT('Ctrl Pts',(0.,-5.08915111884261,8.0227242371374));
#42106=CARTESIAN_POINT('Ctrl Pts',(1.5,-5.08915111884261,8.0227242371374));
#42107=CARTESIAN_POINT('Ctrl Pts',(0.,-5.22746402551034,7.93329585718089));
#42108=CARTESIAN_POINT('Ctrl Pts',(1.5,-5.22746402551034,7.93329585718089));
#42109=CARTESIAN_POINT('Ctrl Pts',(0.,-5.36420586540681,7.84148319732023));
#42110=CARTESIAN_POINT('Ctrl Pts',(1.5,-5.36420586540681,7.84148319732023));
#42111=CARTESIAN_POINT('Ctrl Pts',(0.,-5.4993355418344,7.74731385076152));
#42112=CARTESIAN_POINT('Ctrl Pts',(1.5,-5.4993355418344,7.74731385076152));
#42113=CARTESIAN_POINT('Ctrl Pts',(0.,-5.63281244262548,7.65081611898552));
#42114=CARTESIAN_POINT('Ctrl Pts',(1.5,-5.63281244262548,7.65081611898552));
#42115=CARTESIAN_POINT('Ctrl Pts',(0.,-5.76459645269993,7.55201900375617));
#42116=CARTESIAN_POINT('Ctrl Pts',(1.5,-5.76459645269993,7.55201900375617));
#42117=CARTESIAN_POINT('Ctrl Pts',(0.,-5.89464796575187,7.45095219790274));
#42118=CARTESIAN_POINT('Ctrl Pts',(1.5,-5.89464796575187,7.45095219790274));
#42119=CARTESIAN_POINT('Ctrl Pts',(0.,-6.02292789596841,7.34764607614508));
#42120=CARTESIAN_POINT('Ctrl Pts',(1.5,-6.02292789596841,7.34764607614508));
#42121=CARTESIAN_POINT('Ctrl Pts',(0.,-6.14939768978061,7.24213168596133));
#42122=CARTESIAN_POINT('Ctrl Pts',(1.5,-6.14939768978061,7.24213168596133));
#42123=CARTESIAN_POINT('Ctrl Pts',(0.,-6.27401933764807,7.13444073849797));
#42124=CARTESIAN_POINT('Ctrl Pts',(1.5,-6.27401933764807,7.13444073849797));
#42125=CARTESIAN_POINT('Ctrl Pts',(0.,-6.39675538587714,7.02460559952098));
#42126=CARTESIAN_POINT('Ctrl Pts',(1.5,-6.39675538587714,7.02460559952098));
#42127=CARTESIAN_POINT('Ctrl Pts',(0.,-6.51756894746593,6.91265927922077));
#42128=CARTESIAN_POINT('Ctrl Pts',(1.5,-6.51756894746593,6.91265927922077));
#42129=CARTESIAN_POINT('Ctrl Pts',(0.,-6.63642371298477,6.79863542205745));
#42130=CARTESIAN_POINT('Ctrl Pts',(1.5,-6.63642371298477,6.79863542205745));
#42131=CARTESIAN_POINT('Ctrl Pts',(0.,-6.75328396149252,6.68256829664553));
#42132=CARTESIAN_POINT('Ctrl Pts',(1.5,-6.75328396149252,6.68256829664553));
#42133=CARTESIAN_POINT('Ctrl Pts',(0.,-6.86811457148982,6.56449278567769));
#42134=CARTESIAN_POINT('Ctrl Pts',(1.5,-6.86811457148982,6.56449278567769));
#42135=CARTESIAN_POINT('Ctrl Pts',(0.,-6.98088103190964,6.44444437588688));
#42136=CARTESIAN_POINT('Ctrl Pts',(1.5,-6.98088103190964,6.44444437588688));
#42137=CARTESIAN_POINT('Ctrl Pts',(0.,-7.091549452039,6.32245914695077));
#42138=CARTESIAN_POINT('Ctrl Pts',(1.5,-7.091549452039,6.32245914695077));
#42139=CARTESIAN_POINT('Ctrl Pts',(0.,-7.20008657147919,6.19857376043315));
#42140=CARTESIAN_POINT('Ctrl Pts',(1.5,-7.20008657147919,6.19857376043315));
#42141=CARTESIAN_POINT('Ctrl Pts',(0.,-7.30645977014568,6.07282544876163));
#42142=CARTESIAN_POINT('Ctrl Pts',(1.5,-7.30645977014568,6.07282544876163));
#42143=CARTESIAN_POINT('Ctrl Pts',(0.,-7.41063707830778,5.94525200424091));
#42144=CARTESIAN_POINT('Ctrl Pts',(1.5,-7.41063707830778,5.94525200424091));
#42145=CARTESIAN_POINT('Ctrl Pts',(0.,-7.51258718666891,5.81589176810111));
#42146=CARTESIAN_POINT('Ctrl Pts',(1.5,-7.51258718666891,5.81589176810111));
#42147=CARTESIAN_POINT('Ctrl Pts',(0.,-7.61227945529051,5.68478361858479));
#42148=CARTESIAN_POINT('Ctrl Pts',(1.5,-7.61227945529051,5.68478361858479));
#42149=CARTESIAN_POINT('Ctrl Pts',(0.,-7.70968392255762,5.55196695906749));
#42150=CARTESIAN_POINT('Ctrl Pts',(1.5,-7.70968392255762,5.55196695906749));
#42151=CARTESIAN_POINT('Ctrl Pts',(0.,-7.80477131418672,5.41748170621113));
#42152=CARTESIAN_POINT('Ctrl Pts',(1.5,-7.80477131418672,5.41748170621113));
#42153=CARTESIAN_POINT('Ctrl Pts',(0.,-7.89751305227678,5.28136827814941));
#42154=CARTESIAN_POINT('Ctrl Pts',(1.5,-7.89751305227678,5.28136827814941));
#42155=CARTESIAN_POINT('Ctrl Pts',(0.,-7.98788126440345,5.14366758270466));
#42156=CARTESIAN_POINT('Ctrl Pts',(1.5,-7.98788126440345,5.14366758270466));
#42157=CARTESIAN_POINT('Ctrl Pts',(0.,-8.07584879147818,5.0044210047471));
#42158=CARTESIAN_POINT('Ctrl Pts',(1.5,-8.07584879147818,5.0044210047471));
#42159=CARTESIAN_POINT('Ctrl Pts',(0.,-8.16138919565165,4.86367039358384));
#42160=CARTESIAN_POINT('Ctrl Pts',(1.5,-8.16138919565165,4.86367039358384));
#42161=CARTESIAN_POINT('Ctrl Pts',(0.,-8.24447676826226,4.72145805037682));
#42162=CARTESIAN_POINT('Ctrl Pts',(1.5,-8.24447676826226,4.72145805037682));
#42163=CARTESIAN_POINT('Ctrl Pts',(0.,-8.32508653783021,4.57782671558903));
#42164=CARTESIAN_POINT('Ctrl Pts',(1.5,-8.32508653783021,4.57782671558903));
#42165=CARTESIAN_POINT('Ctrl Pts',(0.,-8.40319427809773,4.43281955645805));
#42166=CARTESIAN_POINT('Ctrl Pts',(1.5,-8.40319427809773,4.43281955645805));
#42167=CARTESIAN_POINT('Ctrl Pts',(0.,-8.47877651476408,4.28648015372245));
#42168=CARTESIAN_POINT('Ctrl Pts',(1.5,-8.47877651476408,4.28648015372245));
#42169=CARTESIAN_POINT('Ctrl Pts',(0.,-8.55181053226761,4.13885248837393));
#42170=CARTESIAN_POINT('Ctrl Pts',(1.5,-8.55181053226761,4.13885248837393));
#42171=CARTESIAN_POINT('Ctrl Pts',(0.,-8.6222743806152,3.98998092843449));
#42172=CARTESIAN_POINT('Ctrl Pts',(1.5,-8.6222743806152,3.98998092843449));
#42173=CARTESIAN_POINT('Ctrl Pts',(0.,-8.69014688225944,3.83991021575771));
#42174=CARTESIAN_POINT('Ctrl Pts',(1.5,-8.69014688225944,3.83991021575771));
#42175=CARTESIAN_POINT('Ctrl Pts',(0.,-8.75540763902411,3.68868545285334));
#42176=CARTESIAN_POINT('Ctrl Pts',(1.5,-8.75540763902411,3.68868545285334));
#42177=CARTESIAN_POINT('Ctrl Pts',(0.,-8.81803703766495,3.53635208908032));
#42178=CARTESIAN_POINT('Ctrl Pts',(1.5,-8.81803703766495,3.53635208908032));
#42179=CARTESIAN_POINT('Ctrl Pts',(0.,-8.87801625547928,3.38295590686148));
#42180=CARTESIAN_POINT('Ctrl Pts',(1.5,-8.87801625547928,3.38295590686148));
#42181=CARTESIAN_POINT('Ctrl Pts',(0.,-8.93532726596516,3.22854300791913));
#42182=CARTESIAN_POINT('Ctrl Pts',(1.5,-8.93532726596516,3.22854300791913));
#42183=CARTESIAN_POINT('Ctrl Pts',(0.,-8.98995284452996,3.07315979953049));
#42184=CARTESIAN_POINT('Ctrl Pts',(1.5,-8.98995284452996,3.07315979953049));
#42185=CARTESIAN_POINT('Ctrl Pts',(0.,-9.04187657424922,2.91685298080215));
#42186=CARTESIAN_POINT('Ctrl Pts',(1.5,-9.04187657424922,2.91685298080215));
#42187=CARTESIAN_POINT('Ctrl Pts',(0.,-9.09108285021124,2.75966952843368));
#42188=CARTESIAN_POINT('Ctrl Pts',(1.5,-9.09108285021124,2.75966952843368));
#42189=CARTESIAN_POINT('Ctrl Pts',(0.,-9.13755688391226,2.60165668249849));
#42190=CARTESIAN_POINT('Ctrl Pts',(1.5,-9.13755688391226,2.60165668249849));
#42191=CARTESIAN_POINT('Ctrl Pts',(0.,-9.18128470770249,2.44286193224103));
#42192=CARTESIAN_POINT('Ctrl Pts',(1.5,-9.18128470770249,2.44286193224103));
#42193=CARTESIAN_POINT('Ctrl Pts',(0.,-9.2222531792836,2.28333300188963));
#42194=CARTESIAN_POINT('Ctrl Pts',(1.5,-9.2222531792836,2.28333300188963));
#42195=CARTESIAN_POINT('Ctrl Pts',(0.,-9.26044998625764,2.12311783648397));
#42196=CARTESIAN_POINT('Ctrl Pts',(1.5,-9.26044998625764,2.12311783648397));
#42197=CARTESIAN_POINT('Ctrl Pts',(0.,-9.29586364922275,1.96226458731596));
#42198=CARTESIAN_POINT('Ctrl Pts',(1.5,-9.29586364922275,1.96226458731596));
#42199=CARTESIAN_POINT('Ctrl Pts',(0.,-9.32848352492098,1.80082159738338));
#42200=CARTESIAN_POINT('Ctrl Pts',(1.5,-9.32848352492098,1.80082159738338));
#42201=CARTESIAN_POINT('Ctrl Pts',(0.,-9.35829980943804,1.63883738685563));
#42202=CARTESIAN_POINT('Ctrl Pts',(1.5,-9.35829980943804,1.63883738685563));
#42203=CARTESIAN_POINT('Ctrl Pts',(0.,-9.38530354145569,1.47636063855043));
#42204=CARTESIAN_POINT('Ctrl Pts',(1.5,-9.38530354145569,1.47636063855043));
#42205=CARTESIAN_POINT('Ctrl Pts',(0.,-9.40948660555648,1.31344018342081));
#42206=CARTESIAN_POINT('Ctrl Pts',(1.5,-9.40948660555648,1.31344018342081));
#42207=CARTESIAN_POINT('Ctrl Pts',(0.,-9.43084173404745,1.15012498578247));
#42208=CARTESIAN_POINT('Ctrl Pts',(1.5,-9.43084173404745,1.15012498578247));
#42209=CARTESIAN_POINT('Ctrl Pts',(0.,-9.44936250883668,0.986464128549687));
#42210=CARTESIAN_POINT('Ctrl Pts',(1.5,-9.44936250883668,0.986464128549687));
#42211=CARTESIAN_POINT('Ctrl Pts',(0.,-9.46504336336294,0.822506798478501));
#42212=CARTESIAN_POINT('Ctrl Pts',(1.5,-9.46504336336294,0.822506798478501));
#42213=CARTESIAN_POINT('Ctrl Pts',(0.,-9.4778795845785,0.658302271416469));
#42214=CARTESIAN_POINT('Ctrl Pts',(1.5,-9.4778795845785,0.658302271416469));
#42215=CARTESIAN_POINT('Ctrl Pts',(0.,-9.48786731498507,0.493899897557971));
#42216=CARTESIAN_POINT('Ctrl Pts',(1.5,-9.48786731498507,0.493899897557971));
#42217=CARTESIAN_POINT('Ctrl Pts',(0.,-9.49500355317182,0.329349086569191));
#42218=CARTESIAN_POINT('Ctrl Pts',(1.5,-9.49500355317182,0.329349086569191));
#42219=CARTESIAN_POINT('Ctrl Pts',(0.,-9.49928615440655,0.164699292716903));
#42220=CARTESIAN_POINT('Ctrl Pts',(1.5,-9.49928615440655,0.164699292716903));
#42221=CARTESIAN_POINT('Ctrl Pts',(0.,-9.50071383128047,6.88023856637576E-14));
#42222=CARTESIAN_POINT('Ctrl Pts',(1.5,-9.50071383128047,6.88023856637576E-14));
#42223=CARTESIAN_POINT('Ctrl Pts',(0.,-9.49928615440671,-0.164699292716751));
#42224=CARTESIAN_POINT('Ctrl Pts',(1.5,-9.49928615440671,-0.164699292716751));
#42225=CARTESIAN_POINT('Ctrl Pts',(0.,-9.49500355317206,-0.329349086569028));
#42226=CARTESIAN_POINT('Ctrl Pts',(1.5,-9.49500355317206,-0.329349086569028));
#42227=CARTESIAN_POINT('Ctrl Pts',(0.,-9.48786731498525,-0.493899897557803));
#42228=CARTESIAN_POINT('Ctrl Pts',(1.5,-9.48786731498525,-0.493899897557803));
#42229=CARTESIAN_POINT('Ctrl Pts',(0.,-9.4778795845786,-0.658302271416311));
#42230=CARTESIAN_POINT('Ctrl Pts',(1.5,-9.4778795845786,-0.658302271416311));
#42231=CARTESIAN_POINT('Ctrl Pts',(0.,-9.46504336336295,-0.822506798478354));
#42232=CARTESIAN_POINT('Ctrl Pts',(1.5,-9.46504336336295,-0.822506798478354));
#42233=CARTESIAN_POINT('Ctrl Pts',(0.,-9.44936250883662,-0.986464128549568));
#42234=CARTESIAN_POINT('Ctrl Pts',(1.5,-9.44936250883662,-0.986464128549568));
#42235=CARTESIAN_POINT('Ctrl Pts',(0.,-9.43084173404737,-1.15012498578238));
#42236=CARTESIAN_POINT('Ctrl Pts',(1.5,-9.43084173404737,-1.15012498578238));
#42237=CARTESIAN_POINT('Ctrl Pts',(0.,-9.40948660555644,-1.31344018342071));
#42238=CARTESIAN_POINT('Ctrl Pts',(1.5,-9.40948660555644,-1.31344018342071));
#42239=CARTESIAN_POINT('Ctrl Pts',(0.,-9.38530354145571,-1.47636063855032));
#42240=CARTESIAN_POINT('Ctrl Pts',(1.5,-9.38530354145571,-1.47636063855032));
#42241=CARTESIAN_POINT('Ctrl Pts',(0.,-9.35829980943809,-1.63883738685548));
#42242=CARTESIAN_POINT('Ctrl Pts',(1.5,-9.35829980943809,-1.63883738685548));
#42243=CARTESIAN_POINT('Ctrl Pts',(0.,-9.32848352492095,-1.80082159738323));
#42244=CARTESIAN_POINT('Ctrl Pts',(1.5,-9.32848352492095,-1.80082159738323));
#42245=CARTESIAN_POINT('Ctrl Pts',(0.,-9.29586364922265,-1.96226458731583));
#42246=CARTESIAN_POINT('Ctrl Pts',(1.5,-9.29586364922265,-1.96226458731583));
#42247=CARTESIAN_POINT('Ctrl Pts',(0.,-9.26044998625752,-2.12311783648386));
#42248=CARTESIAN_POINT('Ctrl Pts',(1.5,-9.26044998625752,-2.12311783648386));
#42249=CARTESIAN_POINT('Ctrl Pts',(0.,-9.22225317928356,-2.28333300188952));
#42250=CARTESIAN_POINT('Ctrl Pts',(1.5,-9.22225317928356,-2.28333300188952));
#42251=CARTESIAN_POINT('Ctrl Pts',(0.,-9.18128470770254,-2.44286193224091));
#42252=CARTESIAN_POINT('Ctrl Pts',(1.5,-9.18128470770254,-2.44286193224091));
#42253=CARTESIAN_POINT('Ctrl Pts',(0.,-9.13755688391234,-2.60165668249832));
#42254=CARTESIAN_POINT('Ctrl Pts',(1.5,-9.13755688391234,-2.60165668249832));
#42255=CARTESIAN_POINT('Ctrl Pts',(0.,-9.09108285021127,-2.75966952843345));
#42256=CARTESIAN_POINT('Ctrl Pts',(1.5,-9.09108285021127,-2.75966952843345));
#42257=CARTESIAN_POINT('Ctrl Pts',(0.,-9.04187657424916,-2.91685298080189));
#42258=CARTESIAN_POINT('Ctrl Pts',(1.5,-9.04187657424916,-2.91685298080189));
#42259=CARTESIAN_POINT('Ctrl Pts',(0.,-8.9899528445299,-3.07315979953029));
#42260=CARTESIAN_POINT('Ctrl Pts',(1.5,-8.9899528445299,-3.07315979953029));
#42261=CARTESIAN_POINT('Ctrl Pts',(0.,-8.9353272659652,-3.22854300791901));
#42262=CARTESIAN_POINT('Ctrl Pts',(1.5,-8.9353272659652,-3.22854300791901));
#42263=CARTESIAN_POINT('Ctrl Pts',(0.,-8.87801625547945,-3.38295590686141));
#42264=CARTESIAN_POINT('Ctrl Pts',(1.5,-8.87801625547945,-3.38295590686141));
#42265=CARTESIAN_POINT('Ctrl Pts',(0.,-8.81803703766518,-3.53635208908027));
#42266=CARTESIAN_POINT('Ctrl Pts',(1.5,-8.81803703766518,-3.53635208908027));
#42267=CARTESIAN_POINT('Ctrl Pts',(0.,-8.75540763902434,-3.68868545285331));
#42268=CARTESIAN_POINT('Ctrl Pts',(1.5,-8.75540763902434,-3.68868545285331));
#42269=CARTESIAN_POINT('Ctrl Pts',(0.,-8.6901468822596,-3.83991021575765));
#42270=CARTESIAN_POINT('Ctrl Pts',(1.5,-8.6901468822596,-3.83991021575765));
#42271=CARTESIAN_POINT('Ctrl Pts',(0.,-8.62227438061525,-3.98998092843437));
#42272=CARTESIAN_POINT('Ctrl Pts',(1.5,-8.62227438061525,-3.98998092843437));
#42273=CARTESIAN_POINT('Ctrl Pts',(0.,-8.55181053226757,-4.13885248837375));
#42274=CARTESIAN_POINT('Ctrl Pts',(1.5,-8.55181053226757,-4.13885248837375));
#42275=CARTESIAN_POINT('Ctrl Pts',(0.,-8.47877651476402,-4.28648015372226));
#42276=CARTESIAN_POINT('Ctrl Pts',(1.5,-8.47877651476402,-4.28648015372226));
#42277=CARTESIAN_POINT('Ctrl Pts',(0.,-8.40319427809771,-4.43281955645792));
#42278=CARTESIAN_POINT('Ctrl Pts',(1.5,-8.40319427809771,-4.43281955645792));
#42279=CARTESIAN_POINT('Ctrl Pts',(0.,-8.32508653783024,-4.57782671558895));
#42280=CARTESIAN_POINT('Ctrl Pts',(1.5,-8.32508653783024,-4.57782671558895));
#42281=CARTESIAN_POINT('Ctrl Pts',(0.,-8.24447676826233,-4.72145805037673));
#42282=CARTESIAN_POINT('Ctrl Pts',(1.5,-8.24447676826233,-4.72145805037673));
#42283=CARTESIAN_POINT('Ctrl Pts',(0.,-8.16138919565173,-4.86367039358363));
#42284=CARTESIAN_POINT('Ctrl Pts',(1.5,-8.16138919565173,-4.86367039358363));
#42285=CARTESIAN_POINT('Ctrl Pts',(0.,-8.07584879147822,-5.00442100474676));
#42286=CARTESIAN_POINT('Ctrl Pts',(1.5,-8.07584879147822,-5.00442100474676));
#42287=CARTESIAN_POINT('Ctrl Pts',(0.,-7.98788126440344,-5.14366758270425));
#42288=CARTESIAN_POINT('Ctrl Pts',(1.5,-7.98788126440344,-5.14366758270425));
#42289=CARTESIAN_POINT('Ctrl Pts',(0.,-7.89751305227676,-5.28136827814908));
#42290=CARTESIAN_POINT('Ctrl Pts',(1.5,-7.89751305227676,-5.28136827814908));
#42291=CARTESIAN_POINT('Ctrl Pts',(0.,-7.80477131418679,-5.41748170621101));
#42292=CARTESIAN_POINT('Ctrl Pts',(1.5,-7.80477131418679,-5.41748170621101));
#42293=CARTESIAN_POINT('Ctrl Pts',(0.,-7.7096839225578,-5.55196695906763));
#42294=CARTESIAN_POINT('Ctrl Pts',(1.5,-7.7096839225578,-5.55196695906763));
#42295=CARTESIAN_POINT('Ctrl Pts',(0.,-7.61227945529079,-5.68478361858509));
#42296=CARTESIAN_POINT('Ctrl Pts',(1.5,-7.61227945529079,-5.68478361858509));
#42297=CARTESIAN_POINT('Ctrl Pts',(0.,-7.51258718666918,-5.81589176810141));
#42298=CARTESIAN_POINT('Ctrl Pts',(1.5,-7.51258718666918,-5.81589176810141));
#42299=CARTESIAN_POINT('Ctrl Pts',(0.,-7.41063707830798,-5.94525200424106));
#42300=CARTESIAN_POINT('Ctrl Pts',(1.5,-7.41063707830798,-5.94525200424106));
#42301=CARTESIAN_POINT('Ctrl Pts',(0.,-7.30645977014577,-6.07282544876153));
#42302=CARTESIAN_POINT('Ctrl Pts',(1.5,-7.30645977014577,-6.07282544876153));
#42303=CARTESIAN_POINT('Ctrl Pts',(0.,-7.20008657147914,-6.19857376043277));
#42304=CARTESIAN_POINT('Ctrl Pts',(1.5,-7.20008657147914,-6.19857376043277));
#42305=CARTESIAN_POINT('Ctrl Pts',(0.,-7.09154945203894,-6.32245914695025));
#42306=CARTESIAN_POINT('Ctrl Pts',(1.5,-7.09154945203894,-6.32245914695025));
#42307=CARTESIAN_POINT('Ctrl Pts',(0.,-6.98088103190963,-6.44444437588636));
#42308=CARTESIAN_POINT('Ctrl Pts',(1.5,-6.98088103190963,-6.44444437588636));
#42309=CARTESIAN_POINT('Ctrl Pts',(0.,-6.86811457148987,-6.56449278567735));
#42310=CARTESIAN_POINT('Ctrl Pts',(1.5,-6.86811457148987,-6.56449278567735));
#42311=CARTESIAN_POINT('Ctrl Pts',(0.,-6.75328396149262,-6.68256829664545));
#42312=CARTESIAN_POINT('Ctrl Pts',(1.5,-6.75328396149262,-6.68256829664545));
#42313=CARTESIAN_POINT('Ctrl Pts',(0.,-6.63642371298489,-6.79863542205757));
#42314=CARTESIAN_POINT('Ctrl Pts',(1.5,-6.63642371298489,-6.79863542205757));
#42315=CARTESIAN_POINT('Ctrl Pts',(0.,-6.51756894746606,-6.91265927922096));
#42316=CARTESIAN_POINT('Ctrl Pts',(1.5,-6.51756894746606,-6.91265927922096));
#42317=CARTESIAN_POINT('Ctrl Pts',(0.,-6.39675538587726,-7.02460559952114));
#42318=CARTESIAN_POINT('Ctrl Pts',(1.5,-6.39675538587726,-7.02460559952114));
#42319=CARTESIAN_POINT('Ctrl Pts',(0.,-6.27401933764821,-7.13444073849804));
#42320=CARTESIAN_POINT('Ctrl Pts',(1.5,-6.27401933764821,-7.13444073849804));
#42321=CARTESIAN_POINT('Ctrl Pts',(0.,-6.14939768978072,-7.24213168596124));
#42322=CARTESIAN_POINT('Ctrl Pts',(1.5,-6.14939768978072,-7.24213168596124));
#42323=CARTESIAN_POINT('Ctrl Pts',(0.,-6.02292789596846,-7.34764607614482));
#42324=CARTESIAN_POINT('Ctrl Pts',(1.5,-6.02292789596846,-7.34764607614482));
#42325=CARTESIAN_POINT('Ctrl Pts',(0.,-5.89464796575191,-7.45095219790239));
#42326=CARTESIAN_POINT('Ctrl Pts',(1.5,-5.89464796575191,-7.45095219790239));
#42327=CARTESIAN_POINT('Ctrl Pts',(0.,-5.76459645269994,-7.55201900375578));
#42328=CARTESIAN_POINT('Ctrl Pts',(1.5,-5.76459645269994,-7.55201900375578));
#42329=CARTESIAN_POINT('Ctrl Pts',(0.,-5.63281244262552,-7.65081611898521));
#42330=CARTESIAN_POINT('Ctrl Pts',(1.5,-5.63281244262552,-7.65081611898521));
#42331=CARTESIAN_POINT('Ctrl Pts',(0.,-5.4993355418345,-7.74731385076143));
#42332=CARTESIAN_POINT('Ctrl Pts',(1.5,-5.4993355418345,-7.74731385076143));
#42333=CARTESIAN_POINT('Ctrl Pts',(0.,-5.36420586540701,-7.84148319732041));
#42334=CARTESIAN_POINT('Ctrl Pts',(1.5,-5.36420586540701,-7.84148319732041));
#42335=CARTESIAN_POINT('Ctrl Pts',(0.,-5.22746402551057,-7.93329585718124));
#42336=CARTESIAN_POINT('Ctrl Pts',(1.5,-5.22746402551057,-7.93329585718124));
#42337=CARTESIAN_POINT('Ctrl Pts',(0.,-5.08915111884281,-8.02272423713777));
#42338=CARTESIAN_POINT('Ctrl Pts',(1.5,-5.08915111884281,-8.02272423713777));
#42339=CARTESIAN_POINT('Ctrl Pts',(0.,-4.94930871410428,-8.1097414602944));
#42340=CARTESIAN_POINT('Ctrl Pts',(1.5,-4.94930871410428,-8.1097414602944));
#42341=CARTESIAN_POINT('Ctrl Pts',(0.,-4.80797883950082,-8.19432137414666));
#42342=CARTESIAN_POINT('Ctrl Pts',(1.5,-4.80797883950082,-8.19432137414666));
#42343=CARTESIAN_POINT('Ctrl Pts',(0.,-4.66520397027463,-8.27643855870703));
#42344=CARTESIAN_POINT('Ctrl Pts',(1.5,-4.66520397027463,-8.27643855870703));
#42345=CARTESIAN_POINT('Ctrl Pts',(0.,-4.52102701626329,-8.35606833467635));
#42346=CARTESIAN_POINT('Ctrl Pts',(1.5,-4.52102701626329,-8.35606833467635));
#42347=CARTESIAN_POINT('Ctrl Pts',(0.,-4.37549130869765,-8.43318677031836));
#42348=CARTESIAN_POINT('Ctrl Pts',(1.5,-4.37549130869765,-8.43318677031836));
#42349=CARTESIAN_POINT('Ctrl Pts',(0.,-4.22864058702611,-8.50777068838071));
#42350=CARTESIAN_POINT('Ctrl Pts',(1.5,-4.22864058702611,-8.50777068838071));
#42351=CARTESIAN_POINT('Ctrl Pts',(0.,-4.08051898576436,-8.57979767306315));
#42352=CARTESIAN_POINT('Ctrl Pts',(1.5,-4.08051898576436,-8.57979767306315));
#42353=CARTESIAN_POINT('Ctrl Pts',(0.,-3.93117102136977,-8.64924607703331));
#42354=CARTESIAN_POINT('Ctrl Pts',(1.5,-3.93117102136977,-8.64924607703331));
#42355=CARTESIAN_POINT('Ctrl Pts',(0.,-3.78064157913962,-8.71609502849035));
#42356=CARTESIAN_POINT('Ctrl Pts',(1.5,-3.78064157913962,-8.71609502849035));
#42357=CARTESIAN_POINT('Ctrl Pts',(0.,-3.62897589946344,-8.78032443687085));
#42358=CARTESIAN_POINT('Ctrl Pts',(1.5,-3.62897589946344,-8.78032443687085));
#42359=CARTESIAN_POINT('Ctrl Pts',(0.,-3.47621956409764,-8.84191499860338));
#42360=CARTESIAN_POINT('Ctrl Pts',(1.5,-3.47621956409764,-8.84191499860338));
#42361=CARTESIAN_POINT('Ctrl Pts',(0.,-3.32241848246127,-8.90084820291222));
#42362=CARTESIAN_POINT('Ctrl Pts',(1.5,-3.32241848246127,-8.90084820291222));
#42363=CARTESIAN_POINT('Ctrl Pts',(0.,-3.16761887795243,-8.95710633767057));
#42364=CARTESIAN_POINT('Ctrl Pts',(1.5,-3.16761887795243,-8.95710633767057));
#42365=CARTESIAN_POINT('Ctrl Pts',(0.,-3.01186727428406,-9.01067249530362));
#42366=CARTESIAN_POINT('Ctrl Pts',(1.5,-3.01186727428406,-9.01067249530362));
#42367=CARTESIAN_POINT('Ctrl Pts',(0.,-2.85521048129404,-9.06153057728234));
#42368=CARTESIAN_POINT('Ctrl Pts',(1.5,-2.85521048129404,-9.06153057728234));
#42369=CARTESIAN_POINT('Ctrl Pts',(0.,-2.69769558077302,-9.10966529866801));
#42370=CARTESIAN_POINT('Ctrl Pts',(1.5,-2.69769558077302,-9.10966529866801));
#42371=CARTESIAN_POINT('Ctrl Pts',(0.,-2.53936991230932,-9.15506219270726));
#42372=CARTESIAN_POINT('Ctrl Pts',(1.5,-2.53936991230932,-9.15506219270726));
#42373=CARTESIAN_POINT('Ctrl Pts',(0.,-2.38028105914982,-9.19770761547843));
#42374=CARTESIAN_POINT('Ctrl Pts',(1.5,-2.38028105914982,-9.19770761547843));
#42375=CARTESIAN_POINT('Ctrl Pts',(0.,-2.22047683407611,-9.23758875058925));
#42376=CARTESIAN_POINT('Ctrl Pts',(1.5,-2.22047683407611,-9.23758875058925));
#42377=CARTESIAN_POINT('Ctrl Pts',(0.,-2.06000526487878,-9.27469361242608));
#42378=CARTESIAN_POINT('Ctrl Pts',(1.5,-2.06000526487878,-9.27469361242608));
#42379=CARTESIAN_POINT('Ctrl Pts',(0.,-1.89891457984506,-9.30901104945512));
#42380=CARTESIAN_POINT('Ctrl Pts',(1.5,-1.89891457984506,-9.30901104945512));
#42381=CARTESIAN_POINT('Ctrl Pts',(0.,-1.73725319325908,-9.34053074757563));
#42382=CARTESIAN_POINT('Ctrl Pts',(1.5,-1.73725319325908,-9.34053074757563));
#42383=CARTESIAN_POINT('Ctrl Pts',(0.,-1.57506969091364,-9.36924323352547));
#42384=CARTESIAN_POINT('Ctrl Pts',(1.5,-1.57506969091364,-9.36924323352547));
#42385=CARTESIAN_POINT('Ctrl Pts',(0.,-1.41241281563273,-9.39513987833904));
#42386=CARTESIAN_POINT('Ctrl Pts',(1.5,-1.41241281563273,-9.39513987833904));
#42387=CARTESIAN_POINT('Ctrl Pts',(0.,-1.249331452519,-9.41821289932504));
#42388=CARTESIAN_POINT('Ctrl Pts',(1.5,-1.249331452519,-9.41821289932504));
#42389=CARTESIAN_POINT('Ctrl Pts',(0.,-1.08587461421005,-9.43845536209718));
#42390=CARTESIAN_POINT('Ctrl Pts',(1.5,-1.08587461421005,-9.43845536209718));
#42391=CARTESIAN_POINT('Ctrl Pts',(0.,-0.922091426142751,-9.45586118265774));
#42392=CARTESIAN_POINT('Ctrl Pts',(1.5,-0.922091426142751,-9.45586118265774));
#42393=CARTESIAN_POINT('Ctrl Pts',(0.,-0.758031111824466,-9.47042512953444));
#42394=CARTESIAN_POINT('Ctrl Pts',(1.5,-0.758031111824466,-9.47042512953444));
#42395=CARTESIAN_POINT('Ctrl Pts',(0.,-0.593742978110514,-9.48214282597024));
#42396=CARTESIAN_POINT('Ctrl Pts',(1.5,-0.593742978110514,-9.48214282597024));
#42397=CARTESIAN_POINT('Ctrl Pts',(0.,-0.429276400335928,-9.49101075062059));
#42398=CARTESIAN_POINT('Ctrl Pts',(1.5,-0.429276400335928,-9.49101075062059));
#42399=CARTESIAN_POINT('Ctrl Pts',(0.,-0.264680807451509,-9.49702623830412));
#42400=CARTESIAN_POINT('Ctrl Pts',(1.5,-0.264680807451509,-9.49702623830412));
#42401=CARTESIAN_POINT('Ctrl Pts',(0.,-0.100005667163201,-9.50018748080672));
#42402=CARTESIAN_POINT('Ctrl Pts',(1.5,-0.100005667163201,-9.50018748080672));
#42403=CARTESIAN_POINT('Ctrl Pts',(0.,0.0646995289261013,-9.5004935277391));
#42404=CARTESIAN_POINT('Ctrl Pts',(1.5,0.0646995289261013,-9.5004935277391));
#42405=CARTESIAN_POINT('Ctrl Pts',(0.,0.229385280173316,-9.49794428744803));
#42406=CARTESIAN_POINT('Ctrl Pts',(1.5,0.229385280173316,-9.49794428744803));
#42407=CARTESIAN_POINT('Ctrl Pts',(0.,0.394002091768334,-9.49254052641434));
#42408=CARTESIAN_POINT('Ctrl Pts',(1.5,0.394002091768334,-9.49254052641434));
#42409=CARTESIAN_POINT('Ctrl Pts',(0.,0.558500489607537,-9.48428386870457));
#42410=CARTESIAN_POINT('Ctrl Pts',(1.5,0.558500489607537,-9.48428386870457));
#42411=CARTESIAN_POINT('Ctrl Pts',(0.,0.722831035168601,-9.47317679547622));
#42412=CARTESIAN_POINT('Ctrl Pts',(1.5,0.722831035168601,-9.47317679547622));
#42413=CARTESIAN_POINT('Ctrl Pts',(0.,0.886944340387529,-9.45922264453641));
#42414=CARTESIAN_POINT('Ctrl Pts',(1.5,0.886944340387529,-9.45922264453641));
#42415=CARTESIAN_POINT('Ctrl Pts',(0.,1.05079108253884,-9.4424256099541));
#42416=CARTESIAN_POINT('Ctrl Pts',(1.5,1.05079108253884,-9.4424256099541));
#42417=CARTESIAN_POINT('Ctrl Pts',(0.,1.21432201899996,-9.42279074019445));
#42418=CARTESIAN_POINT('Ctrl Pts',(1.5,1.21432201899996,-9.42279074019445));
#42419=CARTESIAN_POINT('Ctrl Pts',(0.,1.3774880020205,-9.40032393630669));
#42420=CARTESIAN_POINT('Ctrl Pts',(1.5,1.3774880020205,-9.40032393630669));
#42421=CARTESIAN_POINT('Ctrl Pts',(0.,1.54023999349757,-9.37503195016512));
#42422=CARTESIAN_POINT('Ctrl Pts',(1.5,1.54023999349757,-9.37503195016512));
#42423=CARTESIAN_POINT('Ctrl Pts',(0.,1.70252907975783,-9.34692238276336));
#42424=CARTESIAN_POINT('Ctrl Pts',(1.5,1.70252907975783,-9.34692238276336));
#42425=CARTESIAN_POINT('Ctrl Pts',(0.,1.86430648634745,-9.31600368256141));
#42426=CARTESIAN_POINT('Ctrl Pts',(1.5,1.86430648634745,-9.31600368256141));
#42427=CARTESIAN_POINT('Ctrl Pts',(0.,2.02552359258146,-9.28228514229854));
#42428=CARTESIAN_POINT('Ctrl Pts',(1.5,2.02552359258146,-9.28228514229854));
#42429=CARTESIAN_POINT('Ctrl Pts',(0.,2.18613194610285,-9.24577689585861));
#42430=CARTESIAN_POINT('Ctrl Pts',(1.5,2.18613194610285,-9.24577689585861));
#42431=CARTESIAN_POINT('Ctrl Pts',(0.,2.34608327745199,-9.20648991518806));
#42432=CARTESIAN_POINT('Ctrl Pts',(1.5,2.34608327745199,-9.20648991518806));
#42433=CARTESIAN_POINT('Ctrl Pts',(0.,2.50532951464769,-9.16443600726627));
#42434=CARTESIAN_POINT('Ctrl Pts',(1.5,2.50532951464769,-9.16443600726627));
#42435=CARTESIAN_POINT('Ctrl Pts',(0.,2.66382279778037,-9.11962781112798));
#42436=CARTESIAN_POINT('Ctrl Pts',(1.5,2.66382279778037,-9.11962781112798));
#42437=CARTESIAN_POINT('Ctrl Pts',(0.,2.82151549322629,-9.07207879354574));
#42438=CARTESIAN_POINT('Ctrl Pts',(1.5,2.82151549322629,-9.07207879354574));
#42439=CARTESIAN_POINT('Ctrl Pts',(0.,2.97836020787586,-9.02180324476405));
#42440=CARTESIAN_POINT('Ctrl Pts',(1.5,2.97836020787586,-9.02180324476405));
#42441=CARTESIAN_POINT('Ctrl Pts',(0.,3.13430980337695,-8.96881627428497));
#42442=CARTESIAN_POINT('Ctrl Pts',(1.5,3.13430980337695,-8.96881627428497));
#42443=CARTESIAN_POINT('Ctrl Pts',(0.,3.2893174103942,-8.9131338067048));
#42444=CARTESIAN_POINT('Ctrl Pts',(1.5,3.2893174103942,-8.9131338067048));
#42445=CARTESIAN_POINT('Ctrl Pts',(0.,3.44333644288495,-8.85477257760172));
#42446=CARTESIAN_POINT('Ctrl Pts',(1.5,3.44333644288495,-8.85477257760172));
#42447=CARTESIAN_POINT('Ctrl Pts',(0.,3.59632061189727,-8.79375012773123));
#42448=CARTESIAN_POINT('Ctrl Pts',(1.5,3.59632061189727,-8.79375012773123));
#42449=CARTESIAN_POINT('Ctrl Pts',(0.,3.74822393938631,-8.73008479727211));
#42450=CARTESIAN_POINT('Ctrl Pts',(1.5,3.74822393938631,-8.73008479727211));
#42451=CARTESIAN_POINT('Ctrl Pts',(0.,3.89900077205013,-8.6637957201221));
#42452=CARTESIAN_POINT('Ctrl Pts',(1.5,3.89900077205013,-8.6637957201221));
#42453=CARTESIAN_POINT('Ctrl Pts',(0.,4.04860579518584,-8.59490281824332));
#42454=CARTESIAN_POINT('Ctrl Pts',(1.5,4.04860579518584,-8.59490281824332));
#42455=CARTESIAN_POINT('Ctrl Pts',(0.,4.19699404656678,-8.52342679605681));
#42456=CARTESIAN_POINT('Ctrl Pts',(1.5,4.19699404656678,-8.52342679605681));
#42457=CARTESIAN_POINT('Ctrl Pts',(0.,4.34412092966095,-8.4493891340983));
#42458=CARTESIAN_POINT('Ctrl Pts',(1.5,4.34412092966095,-8.4493891340983));
#42459=CARTESIAN_POINT('Ctrl Pts',(0.,4.48994222687229,-8.37281208272251));
#42460=CARTESIAN_POINT('Ctrl Pts',(1.5,4.48994222687229,-8.37281208272251));
#42461=CARTESIAN_POINT('Ctrl Pts',(0.,4.63441411280551,-8.29371865585542));
#42462=CARTESIAN_POINT('Ctrl Pts',(1.5,4.63441411280551,-8.29371865585542));
#42463=CARTESIAN_POINT('Ctrl Pts',(0.,4.77749316755556,-8.21213262479421));
#42464=CARTESIAN_POINT('Ctrl Pts',(1.5,4.77749316755556,-8.21213262479421));
#42465=CARTESIAN_POINT('Ctrl Pts',(0.,4.91913639002231,-8.12807851205451));
#42466=CARTESIAN_POINT('Ctrl Pts',(1.5,4.91913639002231,-8.12807851205451));
#42467=CARTESIAN_POINT('Ctrl Pts',(0.,5.05930121058847,-8.04158158243562));
#42468=CARTESIAN_POINT('Ctrl Pts',(1.5,5.05930121058847,-8.04158158243562));
#42469=CARTESIAN_POINT('Ctrl Pts',(0.,5.19794550382457,-7.95266783413212));
#42470=CARTESIAN_POINT('Ctrl Pts',(1.5,5.19794550382457,-7.95266783413212));
#42471=CARTESIAN_POINT('Ctrl Pts',(0.,5.33502760122154,-7.86136398989119));
#42472=CARTESIAN_POINT('Ctrl Pts',(1.5,5.33502760122154,-7.86136398989119));
#42473=CARTESIAN_POINT('Ctrl Pts',(0.,5.47050630395188,-7.7676974882153));
#42474=CARTESIAN_POINT('Ctrl Pts',(1.5,5.47050630395188,-7.7676974882153));
#42475=CARTESIAN_POINT('Ctrl Pts',(0.,5.60434089566018,-7.6716964746095));
#42476=CARTESIAN_POINT('Ctrl Pts',(1.5,5.60434089566018,-7.6716964746095));
#42477=CARTESIAN_POINT('Ctrl Pts',(0.,5.73649115418427,-7.57338979499691));
#42478=CARTESIAN_POINT('Ctrl Pts',(1.5,5.73649115418427,-7.57338979499691));
#42479=CARTESIAN_POINT('Ctrl Pts',(0.,5.86691736330717,-7.47280698917772));
#42480=CARTESIAN_POINT('Ctrl Pts',(1.5,5.86691736330717,-7.47280698917772));
#42481=CARTESIAN_POINT('Ctrl Pts',(0.,5.99558032454076,-7.36997828433179));
#42482=CARTESIAN_POINT('Ctrl Pts',(1.5,5.99558032454076,-7.36997828433179));
#42483=CARTESIAN_POINT('Ctrl Pts',(0.,6.1224413689417,-7.26493458856375));
#42484=CARTESIAN_POINT('Ctrl Pts',(1.5,6.1224413689417,-7.26493458856375));
#42485=CARTESIAN_POINT('Ctrl Pts',(0.,6.24746236896048,-7.15770748449079));
#42486=CARTESIAN_POINT('Ctrl Pts',(1.5,6.24746236896048,-7.15770748449079));
#42487=CARTESIAN_POINT('Ctrl Pts',(0.,6.3706057498637,-7.04832921373843));
#42488=CARTESIAN_POINT('Ctrl Pts',(1.5,6.3706057498637,-7.04832921373843));
#42489=CARTESIAN_POINT('Ctrl Pts',(0.,6.49183450119073,-6.93683266147738));
#42490=CARTESIAN_POINT('Ctrl Pts',(1.5,6.49183450119073,-6.93683266147738));
#42491=CARTESIAN_POINT('Ctrl Pts',(0.,6.61111218824578,-6.82325134100072));
#42492=CARTESIAN_POINT('Ctrl Pts',(1.5,6.61111218824578,-6.82325134100072));
#42493=CARTESIAN_POINT('Ctrl Pts',(0.,6.72840296362575,-6.70761937834039));
#42494=CARTESIAN_POINT('Ctrl Pts',(1.5,6.72840296362575,-6.70761937834039));
#42495=CARTESIAN_POINT('Ctrl Pts',(0.,6.84367157878482,-6.58997149692243));
#42496=CARTESIAN_POINT('Ctrl Pts',(1.5,6.84367157878482,-6.58997149692243));
#42497=CARTESIAN_POINT('Ctrl Pts',(0.,6.95688339333968,-6.47034301954872));
#42498=CARTESIAN_POINT('Ctrl Pts',(1.5,6.95688339333968,-6.47034301954872));
#42499=CARTESIAN_POINT('Ctrl Pts',(0.,7.06800438441262,-6.34876987041636));
#42500=CARTESIAN_POINT('Ctrl Pts',(1.5,7.06800438441262,-6.34876987041636));
#42501=CARTESIAN_POINT('Ctrl Pts',(0.,7.17700115601334,-6.22528857717452));
#42502=CARTESIAN_POINT('Ctrl Pts',(1.5,7.17700115601334,-6.22528857717452));
#42503=CARTESIAN_POINT('Ctrl Pts',(0.,7.28384094845988,-6.09993627301844));
#42504=CARTESIAN_POINT('Ctrl Pts',(1.5,7.28384094845988,-6.09993627301844));
#42505=CARTESIAN_POINT('Ctrl Pts',(0.,7.38849164783933,-5.97275069882039));
#42506=CARTESIAN_POINT('Ctrl Pts',(1.5,7.38849164783933,-5.97275069882039));
#42507=CARTESIAN_POINT('Ctrl Pts',(0.,7.49092179714954,-5.84377016152519));
#42508=CARTESIAN_POINT('Ctrl Pts',(1.5,7.49092179714954,-5.84377016152519));
#42509=CARTESIAN_POINT('Ctrl Pts',(0.,7.59110060748179,-5.71303349258081));
#42510=CARTESIAN_POINT('Ctrl Pts',(1.5,7.59110060748179,-5.71303349258081));
#42511=CARTESIAN_POINT('Ctrl Pts',(0.,7.68899796924518,-5.58058000640184));
#42512=CARTESIAN_POINT('Ctrl Pts',(1.5,7.68899796924518,-5.58058000640184));
#42513=CARTESIAN_POINT('Ctrl Pts',(0.,7.78458446343338,-5.44644945886454));
#42514=CARTESIAN_POINT('Ctrl Pts',(1.5,7.78458446343338,-5.44644945886454));
#42515=CARTESIAN_POINT('Ctrl Pts',(0.,7.87783137293427,-5.31068200583085));
#42516=CARTESIAN_POINT('Ctrl Pts',(1.5,7.87783137293427,-5.31068200583085));
#42517=CARTESIAN_POINT('Ctrl Pts',(0.,7.96871068608008,-5.17331826007796));
#42518=CARTESIAN_POINT('Ctrl Pts',(1.5,7.96871068608008,-5.17331826007796));
#42519=CARTESIAN_POINT('Ctrl Pts',(0.,8.05719510024161,-5.03439934825706));
#42520=CARTESIAN_POINT('Ctrl Pts',(1.5,8.05719510024161,-5.03439934825706));
#42521=CARTESIAN_POINT('Ctrl Pts',(0.,8.14325802546676,-4.89396696788343));
#42522=CARTESIAN_POINT('Ctrl Pts',(1.5,8.14325802546676,-4.89396696788343));
#42523=CARTESIAN_POINT('Ctrl Pts',(0.,8.22687358816365,-4.75206344435944));
#42524=CARTESIAN_POINT('Ctrl Pts',(1.5,8.22687358816365,-4.75206344435944));
#42525=CARTESIAN_POINT('Ctrl Pts',(0.,8.30801663482882,-4.60873178803278));
#42526=CARTESIAN_POINT('Ctrl Pts',(1.5,8.30801663482882,-4.60873178803278));
#42527=CARTESIAN_POINT('Ctrl Pts',(0.,8.38666274968152,-4.46401551988012));
#42528=CARTESIAN_POINT('Ctrl Pts',(1.5,8.38666274968152,-4.46401551988012));
#42529=CARTESIAN_POINT('Ctrl Pts',(0.,8.46278827234415,-4.31795849722095));
#42530=CARTESIAN_POINT('Ctrl Pts',(1.5,8.46278827234415,-4.31795849722095));
#42531=CARTESIAN_POINT('Ctrl Pts',(0.,8.53637031556984,-4.17060473945423));
#42532=CARTESIAN_POINT('Ctrl Pts',(1.5,8.53637031556984,-4.17060473945423));
#42533=CARTESIAN_POINT('Ctrl Pts',(0.,8.60738678301777,-4.02199825381128));
#42534=CARTESIAN_POINT('Ctrl Pts',(1.5,8.60738678301777,-4.02199825381128));
#42535=CARTESIAN_POINT('Ctrl Pts',(0.,8.67581638707736,-3.87218286111754));
#42536=CARTESIAN_POINT('Ctrl Pts',(1.5,8.67581638707736,-3.87218286111754));
#42537=CARTESIAN_POINT('Ctrl Pts',(0.,8.74163863005112,-3.7212025564437));
#42538=CARTESIAN_POINT('Ctrl Pts',(1.5,8.74163863005112,-3.7212025564437));
#42539=CARTESIAN_POINT('Ctrl Pts',(0.,8.8048337853866,-3.569101869772));
#42540=CARTESIAN_POINT('Ctrl Pts',(1.5,8.8048337853866,-3.569101869772));
#42541=CARTESIAN_POINT('Ctrl Pts',(0.,8.86538287895677,-3.41592622669153));
#42542=CARTESIAN_POINT('Ctrl Pts',(1.5,8.86538287895677,-3.41592622669153));
#42543=CARTESIAN_POINT('Ctrl Pts',(0.,8.92326767038829,-3.26172230913547));
#42544=CARTESIAN_POINT('Ctrl Pts',(1.5,8.92326767038829,-3.26172230913547));
#42545=CARTESIAN_POINT('Ctrl Pts',(0.,8.97847063443704,-3.10653841617418));
#42546=CARTESIAN_POINT('Ctrl Pts',(1.5,8.97847063443704,-3.10653841617418));
#42547=CARTESIAN_POINT('Ctrl Pts',(0.,9.03097502289857,-2.95042358103383));
#42548=CARTESIAN_POINT('Ctrl Pts',(1.5,9.03097502289857,-2.95042358103383));
#42549=CARTESIAN_POINT('Ctrl Pts',(0.,9.08076492656766,-2.79342668815082));
#42550=CARTESIAN_POINT('Ctrl Pts',(1.5,9.08076492656766,-2.79342668815082));
#42551=CARTESIAN_POINT('Ctrl Pts',(0.,9.12782533724964,-2.63559559022695));
#42552=CARTESIAN_POINT('Ctrl Pts',(1.5,9.12782533724964,-2.63559559022695));
#42553=CARTESIAN_POINT('Ctrl Pts',(0.,9.17214220982579,-2.47697622525295));
#42554=CARTESIAN_POINT('Ctrl Pts',(1.5,9.17214220982579,-2.47697622525295));
#42555=CARTESIAN_POINT('Ctrl Pts',(0.,9.21370252437545,-2.31761173346462));
#42556=CARTESIAN_POINT('Ctrl Pts',(1.5,9.21370252437545,-2.31761173346462));
#42557=CARTESIAN_POINT('Ctrl Pts',(0.,9.25249415711055,-2.15754444747782));
#42558=CARTESIAN_POINT('Ctrl Pts',(1.5,9.25249415711055,-2.15754444747782));
#42559=CARTESIAN_POINT('Ctrl Pts',(0.,9.28850575136439,-1.99681788239702));
#42560=CARTESIAN_POINT('Ctrl Pts',(1.5,9.28850575136439,-1.99681788239702));
#42561=CARTESIAN_POINT('Ctrl Pts',(0.,9.32172658862992,-1.8354787259745));
#42562=CARTESIAN_POINT('Ctrl Pts',(1.5,9.32172658862992,-1.8354787259745));
#42563=CARTESIAN_POINT('Ctrl Pts',(0.,9.35214645964288,-1.67357882889265));
#42564=CARTESIAN_POINT('Ctrl Pts',(1.5,9.35214645964288,-1.67357882889265));
#42565=CARTESIAN_POINT('Ctrl Pts',(0.,9.37975553550456,-1.51117719524876));
#42566=CARTESIAN_POINT('Ctrl Pts',(1.5,9.37975553550456,-1.51117719524876));
#42567=CARTESIAN_POINT('Ctrl Pts',(0.,9.40454466499353,-1.34833562021881));
#42568=CARTESIAN_POINT('Ctrl Pts',(1.5,9.40454466499353,-1.34833562021881));
#42569=CARTESIAN_POINT('Ctrl Pts',(0.,9.42650567192347,-1.18511432783383));
#42570=CARTESIAN_POINT('Ctrl Pts',(1.5,9.42650567192347,-1.18511432783383));
#42571=CARTESIAN_POINT('Ctrl Pts',(0.,9.44563165255895,-1.02156760869846));
#42572=CARTESIAN_POINT('Ctrl Pts',(1.5,9.44563165255895,-1.02156760869846));
#42573=CARTESIAN_POINT('Ctrl Pts',(0.,9.46191727309995,-0.857739457490668));
#42574=CARTESIAN_POINT('Ctrl Pts',(1.5,9.46191727309995,-0.857739457490668));
#42575=CARTESIAN_POINT('Ctrl Pts',(0.,9.475359067247,-0.69365921007208));
#42576=CARTESIAN_POINT('Ctrl Pts',(1.5,9.475359067247,-0.69365921007208));
#42577=CARTESIAN_POINT('Ctrl Pts',(0.,9.48595504112471,-0.529344474234685));
#42578=CARTESIAN_POINT('Ctrl Pts',(1.5,9.48595504112471,-0.529344474234685));
#42579=CARTESIAN_POINT('Ctrl Pts',(0.,9.49215443085059,-0.397712142849856));
#42580=CARTESIAN_POINT('Ctrl Pts',(1.5,9.49215443085059,-0.397712142849856));
#42581=CARTESIAN_POINT('Ctrl Pts',(0.,9.49552283633695,-0.298887663039026));
#42582=CARTESIAN_POINT('Ctrl Pts',(1.5,9.49552283633695,-0.298887663039026));
#42583=CARTESIAN_POINT('Ctrl Pts',(0.,9.49719905300845,-0.232960129825712));
#42584=CARTESIAN_POINT('Ctrl Pts',(1.5,9.49719905300845,-0.232960129825712));
#42585=CARTESIAN_POINT('Ctrl Pts',(0.,9.49789481459768,-0.19998522655085));
#42586=CARTESIAN_POINT('Ctrl Pts',(1.5,9.49789481459768,-0.19998522655085));
#42587=CARTESIAN_POINT('',(0.15,9.49789481459768,0.19998522655078));
#42588=CARTESIAN_POINT('',(0.,9.49789481459768,0.199985226550847));
#42589=CARTESIAN_POINT('Ctrl Pts',(0.15,9.49789467324318,-0.199991925789801));
#42590=CARTESIAN_POINT('Ctrl Pts',(0.15,9.46807533126202,-1.61320182906088));
#42591=CARTESIAN_POINT('Ctrl Pts',(0.15,8.76936042330201,-4.41924950926567));
#42592=CARTESIAN_POINT('Ctrl Pts',(0.15,6.00716218277886,-7.7702406804142));
#42593=CARTESIAN_POINT('Ctrl Pts',(0.15,2.06951231035037,-9.59921473442292));
#42594=CARTESIAN_POINT('Ctrl Pts',(0.15,-2.27052730117003,-9.55414177959014));
#42595=CARTESIAN_POINT('Ctrl Pts',(0.15,-6.16993267085606,-7.64037775456781));
#42596=CARTESIAN_POINT('Ctrl Pts',(0.15,-8.55868308240392,-4.61342308628249));
#42597=CARTESIAN_POINT('Ctrl Pts',(0.15,-9.81741474111766,-0.515781321759936));
#42598=CARTESIAN_POINT('Ctrl Pts',(0.15,-9.23735151866284,3.36699645272176));
#42599=CARTESIAN_POINT('Ctrl Pts',(0.15,-6.56839683600959,7.31525710391206));
#42600=CARTESIAN_POINT('Ctrl Pts',(0.15,-2.7590783122695,9.55398857169003));
#42601=CARTESIAN_POINT('Ctrl Pts',(0.15,2.07186156931854,9.59716037348304));
#42602=CARTESIAN_POINT('Ctrl Pts',(0.15,6.00595373869092,7.771189481248));
#42603=CARTESIAN_POINT('Ctrl Pts',(0.15,8.76999259869694,4.41871090089412));
#42604=CARTESIAN_POINT('Ctrl Pts',(0.15,9.46807646415204,1.61319520738852));
#42605=CARTESIAN_POINT('Ctrl Pts',(0.15,9.49789481459768,0.199985226550645));
#42606=CARTESIAN_POINT('Ctrl Pts',(0.15,9.49789481459768,0.199985226550645));
#42607=CARTESIAN_POINT('Ctrl Pts',(0.15,9.46807646415204,1.61319520738852));
#42608=CARTESIAN_POINT('Ctrl Pts',(0.15,8.76999259869694,4.41871090089412));
#42609=CARTESIAN_POINT('Ctrl Pts',(0.15,6.00595373869092,7.771189481248));
#42610=CARTESIAN_POINT('Ctrl Pts',(0.15,2.07186156931854,9.59716037348304));
#42611=CARTESIAN_POINT('Ctrl Pts',(0.15,-2.7590783122695,9.55398857169003));
#42612=CARTESIAN_POINT('Ctrl Pts',(0.15,-6.56839683600959,7.31525710391206));
#42613=CARTESIAN_POINT('Ctrl Pts',(0.15,-9.23735151866284,3.36699645272176));
#42614=CARTESIAN_POINT('Ctrl Pts',(0.15,-9.81741474111766,-0.515781321759936));
#42615=CARTESIAN_POINT('Ctrl Pts',(0.15,-8.55868308240392,-4.61342308628249));
#42616=CARTESIAN_POINT('Ctrl Pts',(0.15,-6.16993267085606,-7.64037775456781));
#42617=CARTESIAN_POINT('Ctrl Pts',(0.15,-2.27052730117003,-9.55414177959014));
#42618=CARTESIAN_POINT('Ctrl Pts',(0.15,2.06951231035037,-9.59921473442292));
#42619=CARTESIAN_POINT('Ctrl Pts',(0.15,6.00716218277886,-7.7702406804142));
#42620=CARTESIAN_POINT('Ctrl Pts',(0.15,8.76936042330201,-4.41924950926567));
#42621=CARTESIAN_POINT('Ctrl Pts',(0.15,9.46807533126202,-1.61320182906088));
#42622=CARTESIAN_POINT('Ctrl Pts',(0.15,9.49789467324318,-0.199991925789801));
#42623=CARTESIAN_POINT('Ctrl Pts',(0.1,9.44790594084898,0.198930474761433));
#42624=CARTESIAN_POINT('Ctrl Pts',(0.1,9.41824388733793,1.60473292350496));
#42625=CARTESIAN_POINT('Ctrl Pts',(0.1,8.72383591777496,4.39544649470378));
#42626=CARTESIAN_POINT('Ctrl Pts',(0.1,5.97434304623036,7.73029415185335));
#42627=CARTESIAN_POINT('Ctrl Pts',(0.1,2.06095722088225,9.54664763134213));
#42628=CARTESIAN_POINT('Ctrl Pts',(0.1,-2.74455695981483,9.50370569266413));
#42629=CARTESIAN_POINT('Ctrl Pts',(0.1,-6.53382629000873,7.2767554489634));
#42630=CARTESIAN_POINT('Ctrl Pts',(0.1,-9.18873390374524,3.34927559427278));
#42631=CARTESIAN_POINT('Ctrl Pts',(0.1,-9.76574412542408,-0.513066686274358));
#42632=CARTESIAN_POINT('Ctrl Pts',(0.1,-8.51363740045374,-4.58914207119684));
#42633=CARTESIAN_POINT('Ctrl Pts',(0.1,-6.1374592951313,-7.6001648172806));
#42634=CARTESIAN_POINT('Ctrl Pts',(0.1,-2.25857727887409,-9.5038582888179));
#42635=CARTESIAN_POINT('Ctrl Pts',(0.1,2.05862033931887,-9.54869104361738));
#42636=CARTESIAN_POINT('Ctrl Pts',(0.1,5.97554512181216,-7.72935044055577));
#42637=CARTESIAN_POINT('Ctrl Pts',(0.1,8.72320707333466,-4.39598222754933));
#42638=CARTESIAN_POINT('Ctrl Pts',(0.1,9.41824276040486,-1.60473950957998));
#42639=CARTESIAN_POINT('Ctrl Pts',(0.1,9.44790580023542,-0.198937138885166));
#42640=CARTESIAN_POINT('Ctrl Pts',(0.05,9.39791706710029,0.197875722972221));
#42641=CARTESIAN_POINT('Ctrl Pts',(0.05,9.36841131052381,1.5962706396214));
#42642=CARTESIAN_POINT('Ctrl Pts',(0.05,8.67767923685297,4.37218208851344));
#42643=CARTESIAN_POINT('Ctrl Pts',(0.05,5.9427323537698,7.6893988224587));
#42644=CARTESIAN_POINT('Ctrl Pts',(0.05,2.05005287244595,9.49613488920121));
#42645=CARTESIAN_POINT('Ctrl Pts',(0.05,-2.73003560736016,9.45342281363823));
#42646=CARTESIAN_POINT('Ctrl Pts',(0.05,-6.49925574400788,7.23825379401473));
#42647=CARTESIAN_POINT('Ctrl Pts',(0.05,-9.14011628882764,3.3315547358238));
#42648=CARTESIAN_POINT('Ctrl Pts',(0.05,-9.7140735097305,-0.51035205078877));
#42649=CARTESIAN_POINT('Ctrl Pts',(0.05,-8.46859171850355,-4.5648610561112));
#42650=CARTESIAN_POINT('Ctrl Pts',(0.05,-6.10498591940654,-7.55995187999338));
#42651=CARTESIAN_POINT('Ctrl Pts',(0.05,-2.24662725657814,-9.45357479804566));
#42652=CARTESIAN_POINT('Ctrl Pts',(0.05,2.04772836828738,-9.49816735281183));
#42653=CARTESIAN_POINT('Ctrl Pts',(0.05,5.94392806084546,-7.68846020069733));
#42654=CARTESIAN_POINT('Ctrl Pts',(0.05,8.67705372336733,-4.372714945833));
#42655=CARTESIAN_POINT('Ctrl Pts',(0.05,9.3684101895477,-1.59627719009908));
#42656=CARTESIAN_POINT('Ctrl Pts',(0.05,9.39791692722766,-0.197882351980531));
#42657=CARTESIAN_POINT('Ctrl Pts',(0.,9.34792819335159,0.196820971183008));
#42658=CARTESIAN_POINT('Ctrl Pts',(0.,9.3185787337097,1.58780835573784));
#42659=CARTESIAN_POINT('Ctrl Pts',(0.,8.63152255593099,4.34891768232309));
#42660=CARTESIAN_POINT('Ctrl Pts',(0.,5.91112166130923,7.64850349306405));
#42661=CARTESIAN_POINT('Ctrl Pts',(0.,2.03914852400966,9.4456221470603));
#42662=CARTESIAN_POINT('Ctrl Pts',(0.,-2.71551425490549,9.40313993461232));
#42663=CARTESIAN_POINT('Ctrl Pts',(0.,-6.46468519800702,7.19975213906607));
#42664=CARTESIAN_POINT('Ctrl Pts',(0.,-9.09149867391003,3.31383387737481));
#42665=CARTESIAN_POINT('Ctrl Pts',(0.,-9.66240289403692,-0.50763741530319));
#42666=CARTESIAN_POINT('Ctrl Pts',(0.,-8.42354603655337,-4.54058004102555));
#42667=CARTESIAN_POINT('Ctrl Pts',(0.,-6.07251254368177,-7.51973894270617));
#42668=CARTESIAN_POINT('Ctrl Pts',(0.,-2.2346772342822,-9.40329130727341));
#42669=CARTESIAN_POINT('Ctrl Pts',(0.,2.03683639725588,-9.44764366200629));
#42670=CARTESIAN_POINT('Ctrl Pts',(0.,5.91231099987876,-7.64756996083891));
#42671=CARTESIAN_POINT('Ctrl Pts',(0.,8.63090037339999,-4.34944766411667));
#42672=CARTESIAN_POINT('Ctrl Pts',(0.,9.31857761869054,-1.58781487061818));
#42673=CARTESIAN_POINT('Ctrl Pts',(0.,9.3479280542199,-0.196827565075896));
#42674=CARTESIAN_POINT('',(0.,9.34792805421991,0.196827565075895));
#42675=CARTESIAN_POINT('Ctrl Pts',(0.15,9.49789481459768,0.199985226550846));
#42676=CARTESIAN_POINT('Ctrl Pts',(0.1,9.44790594084898,0.198930474761633));
#42677=CARTESIAN_POINT('Ctrl Pts',(0.05,9.39791706710028,0.19787572297242));
#42678=CARTESIAN_POINT('Ctrl Pts',(0.,9.34792819335158,0.196820971183207));
#42679=CARTESIAN_POINT('Ctrl Pts',(0.,9.34792805421987,0.196827565076008));
#42680=CARTESIAN_POINT('Ctrl Pts',(0.,9.31857764805933,1.58781271869574));
#42681=CARTESIAN_POINT('Ctrl Pts',(0.,8.63152112305334,4.34891942026648));
#42682=CARTESIAN_POINT('Ctrl Pts',(0.,5.91112166130923,7.64850349306405));
#42683=CARTESIAN_POINT('Ctrl Pts',(0.,2.03914852400966,9.4456221470603));
#42684=CARTESIAN_POINT('Ctrl Pts',(0.,-2.71551425490549,9.40313993461232));
#42685=CARTESIAN_POINT('Ctrl Pts',(0.,-6.46468519800702,7.19975213906607));
#42686=CARTESIAN_POINT('Ctrl Pts',(0.,-9.09149867391003,3.31383387737481));
#42687=CARTESIAN_POINT('Ctrl Pts',(0.,-9.66240289403692,-0.50763741530319));
#42688=CARTESIAN_POINT('Ctrl Pts',(0.,-8.42354603655337,-4.54058004102555));
#42689=CARTESIAN_POINT('Ctrl Pts',(0.,-6.07251254368177,-7.51973894270617));
#42690=CARTESIAN_POINT('Ctrl Pts',(0.,-2.2346772342822,-9.40329130727341));
#42691=CARTESIAN_POINT('Ctrl Pts',(0.,2.03683639725588,-9.44764366200629));
#42692=CARTESIAN_POINT('Ctrl Pts',(0.,5.91231099987876,-7.64756996083891));
#42693=CARTESIAN_POINT('Ctrl Pts',(0.,8.63090037339999,-4.34944766411667));
#42694=CARTESIAN_POINT('Ctrl Pts',(0.,9.31857761869054,-1.58781487061818));
#42695=CARTESIAN_POINT('Ctrl Pts',(0.,9.3479280542199,-0.196827565075896));
#42696=CARTESIAN_POINT('Ctrl Pts',(1.5,8.14819397266823,-0.171566273307202));
#42697=CARTESIAN_POINT('Ctrl Pts',(1.5,8.13256980638789,-0.912057527264844));
#42698=CARTESIAN_POINT('Ctrl Pts',(1.5,7.82167697943358,-2.8606390589131));
#42699=CARTESIAN_POINT('Ctrl Pts',(1.5,6.2437277562345,-5.63228319243984));
#42700=CARTESIAN_POINT('Ctrl Pts',(1.5,3.27411598702021,-7.75142033677142));
#42701=CARTESIAN_POINT('Ctrl Pts',(1.5,-0.306947971306406,-8.40596108242038));
#42702=CARTESIAN_POINT('Ctrl Pts',(1.5,-3.83187577666327,-7.49038443259283));
#42703=CARTESIAN_POINT('Ctrl Pts',(1.5,-6.63683129723738,-5.16900547712466));
#42704=CARTESIAN_POINT('Ctrl Pts',(1.5,-8.34751515590091,-1.57539769915707));
#42705=CARTESIAN_POINT('Ctrl Pts',(1.5,-8.11584947195258,2.79986176826081));
#42706=CARTESIAN_POINT('Ctrl Pts',(1.5,-5.40342015315134,6.67067944450257));
#42707=CARTESIAN_POINT('Ctrl Pts',(1.5,-1.05510724703267,8.51840124378108));
#42708=CARTESIAN_POINT('Ctrl Pts',(1.5,3.61325431606088,7.78925162987645));
#42709=CARTESIAN_POINT('Ctrl Pts',(1.5,7.18672995402067,4.69400338747101));
#42710=CARTESIAN_POINT('Ctrl Pts',(1.5,8.11619629477138,1.68806323182392));
#42711=CARTESIAN_POINT('Ctrl Pts',(1.5,8.14819383353886,0.171572867200535));
#42712=CARTESIAN_POINT('Ctrl Pts',(1.49821428571429,8.14640865574864,-0.171528603600415));
#42713=CARTESIAN_POINT('Ctrl Pts',(1.49821428571429,8.13078803910471,-0.911854951429866));
#42714=CARTESIAN_POINT('Ctrl Pts',(1.49821428571429,7.81996304417322,-2.86001277316043));
#42715=CARTESIAN_POINT('Ctrl Pts',(1.49821428571429,6.24235987703551,-5.63104745342254));
#42716=CARTESIAN_POINT('Ctrl Pts',(1.49821428571429,3.27339861384903,-7.74972230254187));
#42717=CARTESIAN_POINT('Ctrl Pts',(1.49821428571429,-0.306880734144998,
-8.4041189576045));
#42718=CARTESIAN_POINT('Ctrl Pts',(1.49821428571429,-3.83103616047986,-7.48874329992843));
#42719=CARTESIAN_POINT('Ctrl Pts',(1.49821428571429,-6.63537718766757,-5.16787287967044));
#42720=CARTESIAN_POINT('Ctrl Pts',(1.49821428571429,-8.34568614737968,-1.5750525297584));
#42721=CARTESIAN_POINT('Ctrl Pts',(1.49821428571429,-8.1140712179393,2.79924829077486));
#42722=CARTESIAN_POINT('Ctrl Pts',(1.49821428571429,-5.40223627158938,6.66921785365957));
#42723=CARTESIAN_POINT('Ctrl Pts',(1.49821428571429,-1.05487600617258,8.51653458003634));
#42724=CARTESIAN_POINT('Ctrl Pts',(1.49821428571429,3.61246244976634,7.78754536608789));
#42725=CARTESIAN_POINT('Ctrl Pts',(1.49821428571429,7.18515561436926,4.69297470505487));
#42726=CARTESIAN_POINT('Ctrl Pts',(1.49821428571429,8.11441723405578,1.68769381933928));
#42727=CARTESIAN_POINT('Ctrl Pts',(1.49821428571429,8.14640851661926,0.171535197493771));
#42728=CARTESIAN_POINT('Ctrl Pts',(1.49464285714286,8.14283802190945,-0.171453264186841));
#42729=CARTESIAN_POINT('Ctrl Pts',(1.49464285714286,8.12721912363431,-0.911699781432996));
#42730=CARTESIAN_POINT('Ctrl Pts',(1.49464285714286,7.81653656299143,-2.85870506455113));
#42731=CARTESIAN_POINT('Ctrl Pts',(1.49464285714286,6.23962066743289,-5.6287311498091));
#42732=CARTESIAN_POINT('Ctrl Pts',(1.49464285714286,3.27196431819506,-7.74630401160597));
#42733=CARTESIAN_POINT('Ctrl Pts',(1.49464285714286,-0.306746719965775,
-8.4004583023455));
#42734=CARTESIAN_POINT('Ctrl Pts',(1.49464285714286,-3.8293568117723,-7.48545336015222));
#42735=CARTESIAN_POINT('Ctrl Pts',(1.49464285714286,-6.63246897130202,-5.16561221049837));
#42736=CARTESIAN_POINT('Ctrl Pts',(1.49464285714286,-8.34202811752249,-1.57436032443796));
#42737=CARTESIAN_POINT('Ctrl Pts',(1.49464285714286,-8.11051476861003,2.7980202100795));
#42738=CARTESIAN_POINT('Ctrl Pts',(1.49464285714286,-5.39986843519062,6.66629520618857));
#42739=CARTESIAN_POINT('Ctrl Pts',(1.49464285714286,-1.05441362653318,8.51280133885302));
#42740=CARTESIAN_POINT('Ctrl Pts',(1.49464285714286,3.61087899851321,7.7841326114491));
#42741=CARTESIAN_POINT('Ctrl Pts',(1.49464285714286,7.18200640929766,4.69091743340625));
#42742=CARTESIAN_POINT('Ctrl Pts',(1.49464285714286,8.11086021393872,1.68695621374015));
#42743=CARTESIAN_POINT('Ctrl Pts',(1.49464285714286,8.14283788278007,0.171459858080241));
#42744=CARTESIAN_POINT('Ctrl Pts',(1.48928571428572,8.13748207115066,-0.17134025506648));
#42745=CARTESIAN_POINT('Ctrl Pts',(1.48928571428572,8.12186650547007,-0.911431949339478));
#42746=CARTESIAN_POINT('Ctrl Pts',(1.48928571428571,7.81139664626853,-2.85675123840278));
#42747=CARTESIAN_POINT('Ctrl Pts',(1.48928571428572,6.23551233729744,-5.6252349205191));
#42748=CARTESIAN_POINT('Ctrl Pts',(1.48928571428571,3.26981281147411,-7.74117969343071));
#42749=CARTESIAN_POINT('Ctrl Pts',(1.48928571428572,-0.306545634130199,
-8.39496400872577));
#42750=CARTESIAN_POINT('Ctrl Pts',(1.48928571428571,-3.82683780503573,-7.48051952735625));
#42751=CARTESIAN_POINT('Ctrl Pts',(1.48928571428572,-6.62810664636446,-5.16222057169492));
#42752=CARTESIAN_POINT('Ctrl Pts',(1.48928571428571,-8.33654107453486,-1.57332227836535));
#42753=CARTESIAN_POINT('Ctrl Pts',(1.48928571428572,-8.1051800863798,2.79617824699648));
#42754=CARTESIAN_POINT('Ctrl Pts',(1.48928571428571,-5.39631669087431,6.66191116002174));
#42755=CARTESIAN_POINT('Ctrl Pts',(1.48928571428572,-1.05372004275023,8.50720146496768));
#42756=CARTESIAN_POINT('Ctrl Pts',(1.48928571428571,3.60850378215682,7.77901351135191));
#42757=CARTESIAN_POINT('Ctrl Pts',(1.48928571428572,7.17728267546545,4.68783151285791));
#42758=CARTESIAN_POINT('Ctrl Pts',(1.48928571428572,8.10552452922819,1.68584963424105));
#42759=CARTESIAN_POINT('Ctrl Pts',(1.48928571428572,8.13748193202128,0.171346848959947));
#42760=CARTESIAN_POINT('Ctrl Pts',(1.48392857142857,8.13212612039187,-0.171227245946119));
#42761=CARTESIAN_POINT('Ctrl Pts',(1.48392857142857,8.11651949934755,-0.910903397565355));
#42762=CARTESIAN_POINT('Ctrl Pts',(1.48392857142857,7.80625528052739,-2.85485491778256));
#42763=CARTESIAN_POINT('Ctrl Pts',(1.48392857142857,6.23140760661372,-5.62157685126289));
#42764=CARTESIAN_POINT('Ctrl Pts',(1.48392857142857,3.26766083470535,-7.73607855230273));
#42765=CARTESIAN_POINT('Ctrl Pts',(1.48392857142857,-0.30634406838548,-8.38944510723279));
#42766=CARTESIAN_POINT('Ctrl Pts',(1.48392857142857,-3.82431891963735,-7.47559369866491));
#42767=CARTESIAN_POINT('Ctrl Pts',(1.48392857142857,-6.62374431853364,-5.15882421275128));
#42768=CARTESIAN_POINT('Ctrl Pts',(1.48392857142857,-8.33105404491241,-1.57228617899269));
#42769=CARTESIAN_POINT('Ctrl Pts',(1.48392857142857,-8.09984534293092,2.79433745799257));
#42770=CARTESIAN_POINT('Ctrl Pts',(1.48392857142857,-5.39276502298037,6.65752655669259));
#42771=CARTESIAN_POINT('Ctrl Pts',(1.48392857142857,-1.05302635250161,8.50160150106888));
#42772=CARTESIAN_POINT('Ctrl Pts',(1.48392857142857,3.60612827237966,7.77389464806985));
#42773=CARTESIAN_POINT('Ctrl Pts',(1.48392857142857,7.17255948998649,4.68474549512318));
#42774=CARTESIAN_POINT('Ctrl Pts',(1.48392857142857,8.10018769589636,1.68474178299355));
#42775=CARTESIAN_POINT('Ctrl Pts',(1.48392857142857,8.13212598126249,0.171233839839652));
#42776=CARTESIAN_POINT('Ctrl Pts',(1.47321428571429,8.1214142188743,-0.171001227705398));
#42777=CARTESIAN_POINT('Ctrl Pts',(1.47321428571429,8.1058110766084,-0.910515765059556));
#42778=CARTESIAN_POINT('Ctrl Pts',(1.47321428571429,7.79597626980663,-2.85091461493954));
#42779=CARTESIAN_POINT('Ctrl Pts',(1.47321428571429,6.22318890264251,-5.61467628234092));
#42780=CARTESIAN_POINT('Ctrl Pts',(1.47321428571429,3.26335808814766,-7.72581675646512));
#42781=CARTESIAN_POINT('Ctrl Pts',(1.47321428571429,-0.305942169197622,
-8.37847049187623));
#42782=CARTESIAN_POINT('Ctrl Pts',(1.47321428571429,-3.81928083727071,-7.4657214884944));
#42783=CARTESIAN_POINT('Ctrl Pts',(1.47321428571429,-6.61501967030123,-5.15204361515029));
#42784=CARTESIAN_POINT('Ctrl Pts',(1.47321428571429,-8.32007995134863,-1.57020898154823));
#42785=CARTESIAN_POINT('Ctrl Pts',(1.47321428571429,-8.08917601322925,2.79065286520672));
#42786=CARTESIAN_POINT('Ctrl Pts',(1.47321428571429,-5.38566149095657,6.64875878070508));
#42787=CARTESIAN_POINT('Ctrl Pts',(1.47321428571429,-1.05163924538491,8.49040180440612));
#42788=CARTESIAN_POINT('Ctrl Pts',(1.47321428571429,3.60137800626563,7.76365631341634));
#42789=CARTESIAN_POINT('Ctrl Pts',(1.47321428571429,7.16311171097749,4.67857370920709));
#42790=CARTESIAN_POINT('Ctrl Pts',(1.47321428571429,8.08951697864065,1.68252934606993));
#42791=CARTESIAN_POINT('Ctrl Pts',(1.47321428571429,8.12141407974491,0.171007821599063));
#42792=CARTESIAN_POINT('Ctrl Pts',(1.42857142857143,8.07678129588441,-0.170059485035724));
#42793=CARTESIAN_POINT('Ctrl Pts',(1.42857142857143,8.06123667672408,-0.906855203438805));
#42794=CARTESIAN_POINT('Ctrl Pts',(1.42857142857143,7.75313569047582,-2.83494783500331));
#42795=CARTESIAN_POINT('Ctrl Pts',(1.42857142857143,6.18897254156974,-5.58465422746104));
#42796=CARTESIAN_POINT('Ctrl Pts',(1.42857142857143,3.24542628982086,-7.68324110488138));
#42797=CARTESIAN_POINT('Ctrl Pts',(1.42857142857143,-0.304263824213199,
-8.33254987154725));
#42798=CARTESIAN_POINT('Ctrl Pts',(1.42857142857143,-3.7982897793451,-7.42465007411634));
#42799=CARTESIAN_POINT('Ctrl Pts',(1.42857142857143,-6.57866694663448,-5.12375409419289));
#42800=CARTESIAN_POINT('Ctrl Pts',(1.42857142857143,-8.27435466635361,-1.56156926465683));
#42801=CARTESIAN_POINT('Ctrl Pts',(1.42857142857143,-8.04471999252646,2.77530960627787));
#42802=CARTESIAN_POINT('Ctrl Pts',(1.42857142857143,-5.3560640404145,6.61222200964727));
#42803=CARTESIAN_POINT('Ctrl Pts',(1.42857142857143,-1.04585879714263,8.44373569546135));
#42804=CARTESIAN_POINT('Ctrl Pts',(1.42857142857143,3.58158292881416,7.72099844358104));
#42805=CARTESIAN_POINT('Ctrl Pts',(1.42857142857143,7.12375026710686,4.65285717209956));
#42806=CARTESIAN_POINT('Ctrl Pts',(1.42857142857143,8.04504664545411,1.67330088163032));
#42807=CARTESIAN_POINT('Ctrl Pts',(1.42857142857143,8.07678115675501,0.170066078929943));
#42808=CARTESIAN_POINT('Ctrl Pts',(1.38571428571429,8.03393368981411,-0.169155412072838));
#42809=CARTESIAN_POINT('Ctrl Pts',(1.38571428571429,8.0182385308055,-0.912944788594306));
#42810=CARTESIAN_POINT('Ctrl Pts',(1.38571428571429,7.71206210954355,-2.81750148479799));
#42811=CARTESIAN_POINT('Ctrl Pts',(1.38571428571429,6.15599224754923,-5.56179450124059));
#42812=CARTESIAN_POINT('Ctrl Pts',(1.38571428571429,3.22822907784503,-7.64151474261234));
#42813=CARTESIAN_POINT('Ctrl Pts',(1.38571428571429,-0.302670290692921,
-8.28937251788484));
#42814=CARTESIAN_POINT('Ctrl Pts',(1.38571428571429,-3.77813389419134,-7.38492668159209));
#42815=CARTESIAN_POINT('Ctrl Pts',(1.38571428571429,-6.5437684384882,-5.09677002251735));
#42816=CARTESIAN_POINT('Ctrl Pts',(1.38571428571429,-8.23045790044569,-1.55320342889092));
#42817=CARTESIAN_POINT('Ctrl Pts',(1.38571428571429,-8.00204446766765,2.76053682998459));
#42818=CARTESIAN_POINT('Ctrl Pts',(1.38571428571429,-5.32764767284217,6.5771672327508));
#42819=CARTESIAN_POINT('Ctrl Pts',(1.38571428571429,-1.04031348854024,8.39893954655973));
#42820=CARTESIAN_POINT('Ctrl Pts',(1.38571428571429,3.56259046274421,7.68003816534915));
#42821=CARTESIAN_POINT('Ctrl Pts',(1.38571428571429,7.08594308215698,4.62817287637971));
#42822=CARTESIAN_POINT('Ctrl Pts',(1.38571428571429,8.00239743556643,1.66448840118123));
#42823=CARTESIAN_POINT('Ctrl Pts',(1.38571428571429,8.0339335506847,0.169162005967588));
#42824=CARTESIAN_POINT('Ctrl Pts',(1.35,7.99822735142219,-0.168402017937099));
#42825=CARTESIAN_POINT('Ctrl Pts',(1.35,7.98260318514185,-0.908893271894742));
#42826=CARTESIAN_POINT('Ctrl Pts',(1.35,7.67778340433625,-2.80497576974459));
#42827=CARTESIAN_POINT('Ctrl Pts',(1.35,6.12863466356929,-5.53707972089446));
#42828=CARTESIAN_POINT('Ctrl Pts',(1.35,3.21388161442135,-7.60755405802142));
#42829=CARTESIAN_POINT('Ctrl Pts',(1.35,-0.301325547464756,-8.25253002156739));
#42830=CARTESIAN_POINT('Ctrl Pts',(1.35,-3.76134157052312,-7.35210402830392));
#42831=CARTESIAN_POINT('Ctrl Pts',(1.35,-6.51468624709197,-5.07411807343295));
#42832=CARTESIAN_POINT('Ctrl Pts',(1.35,-8.19387773002112,-1.54630004091758));
#42833=CARTESIAN_POINT('Ctrl Pts',(1.35,-7.96647938740201,2.74826728026557));
#42834=CARTESIAN_POINT('Ctrl Pts',(1.35,-5.30397004160299,6.54793541589078));
#42835=CARTESIAN_POINT('Ctrl Pts',(1.35,-1.0356886713384,8.36160627166494));
#42836=CARTESIAN_POINT('Ctrl Pts',(1.35,3.5467531368535,7.64591288957791));
#42837=CARTESIAN_POINT('Ctrl Pts',(1.35,7.05445628912872,4.60759922805685));
#42838=CARTESIAN_POINT('Ctrl Pts',(1.35,7.9668162212544,1.6571001514885));
#42839=CARTESIAN_POINT('Ctrl Pts',(1.35,7.99822721229278,0.168408611832292));
#42840=CARTESIAN_POINT('',(1.35,7.99822721229278,0.168408611832292));
#42841=CARTESIAN_POINT('',(1.5,8.14819390295858,0.171569570250815));
#42842=CARTESIAN_POINT('Ctrl Pts',(1.35,7.99822721229278,0.168408611832292));
#42843=CARTESIAN_POINT('Ctrl Pts',(1.38571428571429,8.0339335506847,0.169162005967588));
#42844=CARTESIAN_POINT('Ctrl Pts',(1.42857142857143,8.07678115675501,0.170066078929943));
#42845=CARTESIAN_POINT('Ctrl Pts',(1.47321428571429,8.12141407974491,0.171007821599063));
#42846=CARTESIAN_POINT('Ctrl Pts',(1.48392857142857,8.13212598126249,0.171233839839652));
#42847=CARTESIAN_POINT('Ctrl Pts',(1.48928571428572,8.13748193202128,0.171346848959947));
#42848=CARTESIAN_POINT('Ctrl Pts',(1.49464285714286,8.14283788278007,0.171459858080241));
#42849=CARTESIAN_POINT('Ctrl Pts',(1.49821428571429,8.14640851661926,0.171535197493771));
#42850=CARTESIAN_POINT('Ctrl Pts',(1.5,8.14819383353886,0.171572867200535));
#42851=CARTESIAN_POINT('Ctrl Pts',(1.5,8.14819383353886,0.171572867200535));
#42852=CARTESIAN_POINT('Ctrl Pts',(1.5,8.11619629477138,1.68806323182392));
#42853=CARTESIAN_POINT('Ctrl Pts',(1.5,7.18672995402067,4.69400338747101));
#42854=CARTESIAN_POINT('Ctrl Pts',(1.5,3.61325431606088,7.78925162987645));
#42855=CARTESIAN_POINT('Ctrl Pts',(1.5,-1.05510724703267,8.51840124378108));
#42856=CARTESIAN_POINT('Ctrl Pts',(1.5,-5.40342015315134,6.67067944450257));
#42857=CARTESIAN_POINT('Ctrl Pts',(1.5,-8.11584947195258,2.79986176826081));
#42858=CARTESIAN_POINT('Ctrl Pts',(1.5,-8.34751515590091,-1.57539769915707));
#42859=CARTESIAN_POINT('Ctrl Pts',(1.5,-6.63683129723738,-5.16900547712466));
#42860=CARTESIAN_POINT('Ctrl Pts',(1.5,-3.83187577666327,-7.49038443259283));
#42861=CARTESIAN_POINT('Ctrl Pts',(1.5,-0.306947971306406,-8.40596108242038));
#42862=CARTESIAN_POINT('Ctrl Pts',(1.5,3.27411598702021,-7.75142033677142));
#42863=CARTESIAN_POINT('Ctrl Pts',(1.5,6.2437277562345,-5.63228319243984));
#42864=CARTESIAN_POINT('Ctrl Pts',(1.5,7.82167697943358,-2.8606390589131));
#42865=CARTESIAN_POINT('Ctrl Pts',(1.5,8.13256980638789,-0.912057527264844));
#42866=CARTESIAN_POINT('Ctrl Pts',(1.5,8.14819397266823,-0.171566273307202));
#42867=CARTESIAN_POINT('Ctrl Pts',(1.35,7.99822721229006,-0.1684086118322));
#42868=CARTESIAN_POINT('Ctrl Pts',(1.35,7.9826024818273,-0.908897646744252));
#42869=CARTESIAN_POINT('Ctrl Pts',(1.35,7.67778229520457,-2.80497772582728));
#42870=CARTESIAN_POINT('Ctrl Pts',(1.35,6.12863466356929,-5.53707972089446));
#42871=CARTESIAN_POINT('Ctrl Pts',(1.35,3.21388161442135,-7.60755405802142));
#42872=CARTESIAN_POINT('Ctrl Pts',(1.35,-0.301325547464756,-8.25253002156739));
#42873=CARTESIAN_POINT('Ctrl Pts',(1.35,-3.76134157052312,-7.35210402830392));
#42874=CARTESIAN_POINT('Ctrl Pts',(1.35,-6.51468624709197,-5.07411807343295));
#42875=CARTESIAN_POINT('Ctrl Pts',(1.35,-8.19387773002112,-1.54630004091758));
#42876=CARTESIAN_POINT('Ctrl Pts',(1.35,-7.96647938740201,2.74826728026557));
#42877=CARTESIAN_POINT('Ctrl Pts',(1.35,-5.30397004160299,6.54793541589078));
#42878=CARTESIAN_POINT('Ctrl Pts',(1.35,-1.0356886713384,8.36160627166494));
#42879=CARTESIAN_POINT('Ctrl Pts',(1.35,3.5467531368535,7.64591288957791));
#42880=CARTESIAN_POINT('Ctrl Pts',(1.35,7.05445628912872,4.60759922805685));
#42881=CARTESIAN_POINT('Ctrl Pts',(1.35,7.9668162212544,1.6571001514885));
#42882=CARTESIAN_POINT('Ctrl Pts',(1.35,7.99822721229278,0.168408611832292));
#42883=CARTESIAN_POINT('Ctrl Pts',(0.,7.99822721229278,-0.168408611832294));
#42884=CARTESIAN_POINT('Ctrl Pts',(1.5,7.99822721229278,-0.168408611832294));
#42885=CARTESIAN_POINT('Ctrl Pts',(0.,7.99764130779638,-0.196176951432016));
#42886=CARTESIAN_POINT('Ctrl Pts',(1.5,7.99764130779638,-0.196176951432016));
#42887=CARTESIAN_POINT('Ctrl Pts',(0.,7.99622975691477,-0.251694874137705));
#42888=CARTESIAN_POINT('Ctrl Pts',(1.5,7.99622975691477,-0.251694874137705));
#42889=CARTESIAN_POINT('Ctrl Pts',(0.,7.99339320492592,-0.334915488714981));
#42890=CARTESIAN_POINT('Ctrl Pts',(1.5,7.99339320492592,-0.334915488714981));
#42891=CARTESIAN_POINT('Ctrl Pts',(0.,7.98817266620921,-0.445763767775749));
#42892=CARTESIAN_POINT('Ctrl Pts',(1.5,7.98817266620921,-0.445763767775749));
#42893=CARTESIAN_POINT('Ctrl Pts',(0.,7.97924974083877,-0.584134071638914));
#42894=CARTESIAN_POINT('Ctrl Pts',(1.5,7.97924974083877,-0.584134071638914));
#42895=CARTESIAN_POINT('Ctrl Pts',(0.,7.96793033524168,-0.722306911570631));
#42896=CARTESIAN_POINT('Ctrl Pts',(1.5,7.96793033524168,-0.722306911570631));
#42897=CARTESIAN_POINT('Ctrl Pts',(0.,7.95421612847075,-0.860267459956458));
#42898=CARTESIAN_POINT('Ctrl Pts',(1.5,7.95421612847075,-0.860267459956458));
#42899=CARTESIAN_POINT('Ctrl Pts',(0.,7.93811003951485,-0.997991012912835));
#42900=CARTESIAN_POINT('Ctrl Pts',(1.5,7.93811003951485,-0.997991012912835));
#42901=CARTESIAN_POINT('Ctrl Pts',(0.,7.91961655999501,-1.1354405222898));
#42902=CARTESIAN_POINT('Ctrl Pts',(1.5,7.91961655999501,-1.1354405222898));
#42903=CARTESIAN_POINT('Ctrl Pts',(0.,7.89874150358321,-1.27257026968344));
#42904=CARTESIAN_POINT('Ctrl Pts',(1.5,7.89874150358321,-1.27257026968344));
#42905=CARTESIAN_POINT('Ctrl Pts',(0.,7.87549175548901,-1.40932954012024));
#42906=CARTESIAN_POINT('Ctrl Pts',(1.5,7.87549175548901,-1.40932954012024));
#42907=CARTESIAN_POINT('Ctrl Pts',(0.,7.84987502200417,-1.54566629555733));
#42908=CARTESIAN_POINT('Ctrl Pts',(1.5,7.84987502200417,-1.54566629555733));
#42909=CARTESIAN_POINT('Ctrl Pts',(0.,7.82189958009612,-1.68153084833392));
#42910=CARTESIAN_POINT('Ctrl Pts',(1.5,7.82189958009612,-1.68153084833392));
#42911=CARTESIAN_POINT('Ctrl Pts',(0.,7.79157402704011,-1.81687953471755));
#42912=CARTESIAN_POINT('Ctrl Pts',(1.5,7.79157402704011,-1.81687953471755));
#42913=CARTESIAN_POINT('Ctrl Pts',(0.,7.7589073889474,-1.95167303870642));
#42914=CARTESIAN_POINT('Ctrl Pts',(1.5,7.7589073889474,-1.95167303870642));
#42915=CARTESIAN_POINT('Ctrl Pts',(0.,7.72390922932679,-2.08587471600204));
#42916=CARTESIAN_POINT('Ctrl Pts',(1.5,7.72390922932679,-2.08587471600204));
#42917=CARTESIAN_POINT('Ctrl Pts',(0.,7.68658975768396,-2.21944891808571));
#42918=CARTESIAN_POINT('Ctrl Pts',(1.5,7.68658975768396,-2.21944891808571));
#42919=CARTESIAN_POINT('Ctrl Pts',(0.,7.64695993816252,-2.35235931633769));
#42920=CARTESIAN_POINT('Ctrl Pts',(1.5,7.64695993816252,-2.35235931633769));
#42921=CARTESIAN_POINT('Ctrl Pts',(0.,7.60503159823077,-2.48456722613405));
#42922=CARTESIAN_POINT('Ctrl Pts',(1.5,7.60503159823077,-2.48456722613405));
#42923=CARTESIAN_POINT('Ctrl Pts',(0.,7.56081737636842,-2.61603235046274));
#42924=CARTESIAN_POINT('Ctrl Pts',(1.5,7.56081737636842,-2.61603235046274));
#42925=CARTESIAN_POINT('Ctrl Pts',(0.,7.51433066980093,-2.74671352348261));
#42926=CARTESIAN_POINT('Ctrl Pts',(1.5,7.51433066980093,-2.74671352348261));
#42927=CARTESIAN_POINT('Ctrl Pts',(0.,7.46558558227944,-2.87656945405589));
#42928=CARTESIAN_POINT('Ctrl Pts',(1.5,7.46558558227944,-2.87656945405589));
#42929=CARTESIAN_POINT('Ctrl Pts',(0.,7.41459687190435,-3.00555946928131));
#42930=CARTESIAN_POINT('Ctrl Pts',(1.5,7.41459687190435,-3.00555946928131));
#42931=CARTESIAN_POINT('Ctrl Pts',(0.,7.36137989899016,-3.13364425805735));
#42932=CARTESIAN_POINT('Ctrl Pts',(1.5,7.36137989899016,-3.13364425805735));
#42933=CARTESIAN_POINT('Ctrl Pts',(0.,7.30595064174916,-3.26078556725641));
#42934=CARTESIAN_POINT('Ctrl Pts',(1.5,7.30595064174916,-3.26078556725641));
#42935=CARTESIAN_POINT('Ctrl Pts',(0.,7.24832571201489,-3.38694589794601));
#42936=CARTESIAN_POINT('Ctrl Pts',(1.5,7.24832571201489,-3.38694589794601));
#42937=CARTESIAN_POINT('Ctrl Pts',(0.,7.18852237100625,-3.51208820164554));
#42938=CARTESIAN_POINT('Ctrl Pts',(1.5,7.18852237100625,-3.51208820164554));
#42939=CARTESIAN_POINT('Ctrl Pts',(0.,7.1265585451321,-3.63617557660718));
#42940=CARTESIAN_POINT('Ctrl Pts',(1.5,7.1265585451321,-3.63617557660718));
#42941=CARTESIAN_POINT('Ctrl Pts',(0.,7.0624528418373,-3.75917096410974));
#42942=CARTESIAN_POINT('Ctrl Pts',(1.5,7.0624528418373,-3.75917096410974));
#42943=CARTESIAN_POINT('Ctrl Pts',(0.,6.9962245345929,-3.88103729518562));
#42944=CARTESIAN_POINT('Ctrl Pts',(1.5,6.9962245345929,-3.88103729518562));
#42945=CARTESIAN_POINT('Ctrl Pts',(0.,6.92789354792742,-4.00173763735532));
#42946=CARTESIAN_POINT('Ctrl Pts',(1.5,6.92789354792742,-4.00173763735532));
#42947=CARTESIAN_POINT('Ctrl Pts',(0.,6.8574804424984,-4.12123534137538));
#42948=CARTESIAN_POINT('Ctrl Pts',(1.5,6.8574804424984,-4.12123534137538));
#42949=CARTESIAN_POINT('Ctrl Pts',(0.,6.78500640020348,-4.23949418800576));
#42950=CARTESIAN_POINT('Ctrl Pts',(1.5,6.78500640020348,-4.23949418800576));
#42951=CARTESIAN_POINT('Ctrl Pts',(0.,6.7104932093306,-4.35647853480234));
#42952=CARTESIAN_POINT('Ctrl Pts',(1.5,6.7104932093306,-4.35647853480234));
#42953=CARTESIAN_POINT('Ctrl Pts',(0.,6.63396326141838,-4.47215326806802));
#42954=CARTESIAN_POINT('Ctrl Pts',(1.5,6.63396326141838,-4.47215326806802));
#42955=CARTESIAN_POINT('Ctrl Pts',(0.,6.55543954815452,-4.58648375483326));
#42956=CARTESIAN_POINT('Ctrl Pts',(1.5,6.55543954815452,-4.58648375483326));
#42957=CARTESIAN_POINT('Ctrl Pts',(0.,6.47494565831181,-4.69943579486461));
#42958=CARTESIAN_POINT('Ctrl Pts',(1.5,6.47494565831181,-4.69943579486461));
#42959=CARTESIAN_POINT('Ctrl Pts',(0.,6.39250577472155,-4.81097557269941));
#42960=CARTESIAN_POINT('Ctrl Pts',(1.5,6.39250577472155,-4.81097557269941));
#42961=CARTESIAN_POINT('Ctrl Pts',(0.,6.30814467128388,-4.92106960970514));
#42962=CARTESIAN_POINT('Ctrl Pts',(1.5,6.30814467128388,-4.92106960970514));
#42963=CARTESIAN_POINT('Ctrl Pts',(0.,6.2218877034437,-5.02968479900636));
#42964=CARTESIAN_POINT('Ctrl Pts',(1.5,6.2218877034437,-5.02968479900636));
#42965=CARTESIAN_POINT('Ctrl Pts',(0.,6.13376079870311,-5.13678844043638));
#42966=CARTESIAN_POINT('Ctrl Pts',(1.5,6.13376079870311,-5.13678844043638));
#42967=CARTESIAN_POINT('Ctrl Pts',(0.,6.0437904471692,-5.24234827551529));
#42968=CARTESIAN_POINT('Ctrl Pts',(1.5,6.0437904471692,-5.24234827551529));
#42969=CARTESIAN_POINT('Ctrl Pts',(0.,5.9520036921371,-5.34633252245589));
#42970=CARTESIAN_POINT('Ctrl Pts',(1.5,5.9520036921371,-5.34633252245589));
#42971=CARTESIAN_POINT('Ctrl Pts',(0.,5.85842812070735,-5.44870991119904));
#42972=CARTESIAN_POINT('Ctrl Pts',(1.5,5.85842812070735,-5.44870991119904));
#42973=CARTESIAN_POINT('Ctrl Pts',(0.,5.76309185581909,-5.54944968161907));
#42974=CARTESIAN_POINT('Ctrl Pts',(1.5,5.76309185581909,-5.54944968161907));
#42975=CARTESIAN_POINT('Ctrl Pts',(0.,5.66602354831668,-5.64852158176045));
#42976=CARTESIAN_POINT('Ctrl Pts',(1.5,5.66602354831668,-5.64852158176045));
#42977=CARTESIAN_POINT('Ctrl Pts',(0.,5.56725236904917,-5.74589586610578));
#42978=CARTESIAN_POINT('Ctrl Pts',(1.5,5.56725236904917,-5.74589586610578));
#42979=CARTESIAN_POINT('Ctrl Pts',(0.,5.46680800100265,-5.84154329387539));
#42980=CARTESIAN_POINT('Ctrl Pts',(1.5,5.46680800100265,-5.84154329387539));
#42981=CARTESIAN_POINT('Ctrl Pts',(0.,5.36472063146399,-5.93543512735822));
#42982=CARTESIAN_POINT('Ctrl Pts',(1.5,5.36472063146399,-5.93543512735822));
#42983=CARTESIAN_POINT('Ctrl Pts',(0.,5.26102094228231,-6.02754314483389));
#42984=CARTESIAN_POINT('Ctrl Pts',(1.5,5.26102094228231,-6.02754314483389));
#42985=CARTESIAN_POINT('Ctrl Pts',(0.,5.15574010016132,-6.11783965352703));
#42986=CARTESIAN_POINT('Ctrl Pts',(1.5,5.15574010016132,-6.11783965352703));
#42987=CARTESIAN_POINT('Ctrl Pts',(0.,5.04890974698177,-6.20629750259511));
#42988=CARTESIAN_POINT('Ctrl Pts',(1.5,5.04890974698177,-6.20629750259511));
#42989=CARTESIAN_POINT('Ctrl Pts',(0.,4.94056199015376,-6.29289009614986));
#42990=CARTESIAN_POINT('Ctrl Pts',(1.5,4.94056199015376,-6.29289009614986));
#42991=CARTESIAN_POINT('Ctrl Pts',(0.,4.83072939299784,-6.3775914063135));
#42992=CARTESIAN_POINT('Ctrl Pts',(1.5,4.83072939299784,-6.3775914063135));
#42993=CARTESIAN_POINT('Ctrl Pts',(0.,4.71944496476703,-6.46037597861881));
#42994=CARTESIAN_POINT('Ctrl Pts',(1.5,4.71944496476703,-6.46037597861881));
#42995=CARTESIAN_POINT('Ctrl Pts',(0.,4.60674215069668,-6.54121893744458));
#42996=CARTESIAN_POINT('Ctrl Pts',(1.5,4.60674215069668,-6.54121893744458));
#42997=CARTESIAN_POINT('Ctrl Pts',(0.,4.49265482208138,-6.62009599148724));
#42998=CARTESIAN_POINT('Ctrl Pts',(1.5,4.49265482208138,-6.62009599148724));
#42999=CARTESIAN_POINT('Ctrl Pts',(0.,4.37721726637847,-6.69698343926892));
#43000=CARTESIAN_POINT('Ctrl Pts',(1.5,4.37721726637847,-6.69698343926892));
#43001=CARTESIAN_POINT('Ctrl Pts',(0.,4.26046417733745,-6.7718581746823));
#43002=CARTESIAN_POINT('Ctrl Pts',(1.5,4.26046417733745,-6.7718581746823));
#43003=CARTESIAN_POINT('Ctrl Pts',(0.,4.14243064422915,-6.84469769436137));
#43004=CARTESIAN_POINT('Ctrl Pts',(1.5,4.14243064422915,-6.84469769436137));
#43005=CARTESIAN_POINT('Ctrl Pts',(0.,4.02315214109941,-6.91548010508963));
#43006=CARTESIAN_POINT('Ctrl Pts',(1.5,4.02315214109941,-6.91548010508963));
#43007=CARTESIAN_POINT('Ctrl Pts',(0.,3.90266451604688,-6.98418413124661));
#43008=CARTESIAN_POINT('Ctrl Pts',(1.5,3.90266451604688,-6.98418413124661));
#43009=CARTESIAN_POINT('Ctrl Pts',(0.,3.78100398052421,-7.05078912229274));
#43010=CARTESIAN_POINT('Ctrl Pts',(1.5,3.78100398052421,-7.05078912229274));
#43011=CARTESIAN_POINT('Ctrl Pts',(0.,3.658207098662,-7.11527506029345));
#43012=CARTESIAN_POINT('Ctrl Pts',(1.5,3.658207098662,-7.11527506029345));
#43013=CARTESIAN_POINT('Ctrl Pts',(0.,3.53431077605632,-7.17762256510059));
#43014=CARTESIAN_POINT('Ctrl Pts',(1.5,3.53431077605632,-7.17762256510059));
#43015=CARTESIAN_POINT('Ctrl Pts',(0.,3.40935224857761,-7.23781289957334));
#43016=CARTESIAN_POINT('Ctrl Pts',(1.5,3.40935224857761,-7.23781289957334));
#43017=CARTESIAN_POINT('Ctrl Pts',(0.,3.28336907120022,-7.29582797483959));
#43018=CARTESIAN_POINT('Ctrl Pts',(1.5,3.28336907120022,-7.29582797483959));
#43019=CARTESIAN_POINT('Ctrl Pts',(0.,3.15639910685184,-7.35165035559749));
#43020=CARTESIAN_POINT('Ctrl Pts',(1.5,3.15639910685184,-7.35165035559749));
#43021=CARTESIAN_POINT('Ctrl Pts',(0.,3.02848051528223,-7.40526326545788));
#43022=CARTESIAN_POINT('Ctrl Pts',(1.5,3.02848051528223,-7.40526326545788));
#43023=CARTESIAN_POINT('Ctrl Pts',(0.,2.89965174137715,-7.45665059166467));
#43024=CARTESIAN_POINT('Ctrl Pts',(1.5,2.89965174137715,-7.45665059166467));
#43025=CARTESIAN_POINT('Ctrl Pts',(0.,2.76995150349014,-7.50579688985674));
#43026=CARTESIAN_POINT('Ctrl Pts',(1.5,2.76995150349014,-7.50579688985674));
#43027=CARTESIAN_POINT('Ctrl Pts',(0.,2.63941878179125,-7.55268738887152));
#43028=CARTESIAN_POINT('Ctrl Pts',(1.5,2.63941878179125,-7.55268738887152));
#43029=CARTESIAN_POINT('Ctrl Pts',(0.,2.50809280663222,-7.59730799559061));
#43030=CARTESIAN_POINT('Ctrl Pts',(1.5,2.50809280663222,-7.59730799559061));
#43031=CARTESIAN_POINT('Ctrl Pts',(0.,2.37601304692718,-7.63964529982775));
#43032=CARTESIAN_POINT('Ctrl Pts',(1.5,2.37601304692718,-7.63964529982775));
#43033=CARTESIAN_POINT('Ctrl Pts',(0.,2.24321919813061,-7.67968657779174));
#43034=CARTESIAN_POINT('Ctrl Pts',(1.5,2.24321919813061,-7.67968657779174));
#43035=CARTESIAN_POINT('Ctrl Pts',(0.,2.10975117022955,-7.71741979559249));
#43036=CARTESIAN_POINT('Ctrl Pts',(1.5,2.10975117022955,-7.71741979559249));
#43037=CARTESIAN_POINT('Ctrl Pts',(0.,1.97564907574918,-7.7528336127899));
#43038=CARTESIAN_POINT('Ctrl Pts',(1.5,1.97564907574918,-7.7528336127899));
#43039=CARTESIAN_POINT('Ctrl Pts',(0.,1.84095321777114,-7.78591738598633));
#43040=CARTESIAN_POINT('Ctrl Pts',(1.5,1.84095321777114,-7.78591738598633));
#43041=CARTESIAN_POINT('Ctrl Pts',(0.,1.70570407796376,-7.81666117246218));
#43042=CARTESIAN_POINT('Ctrl Pts',(1.5,1.70570407796376,-7.81666117246218));
#43043=CARTESIAN_POINT('Ctrl Pts',(0.,1.56994230429296,-7.84505573268351));
#43044=CARTESIAN_POINT('Ctrl Pts',(1.5,1.56994230429296,-7.84505573268351));
#43045=CARTESIAN_POINT('Ctrl Pts',(0.,1.43370869874369,-7.87109253285344));
#43046=CARTESIAN_POINT('Ctrl Pts',(1.5,1.43370869874369,-7.87109253285344));
#43047=CARTESIAN_POINT('Ctrl Pts',(0.,1.29704420505069,-7.89476374750745));
#43048=CARTESIAN_POINT('Ctrl Pts',(1.5,1.29704420505069,-7.89476374750745));
#43049=CARTESIAN_POINT('Ctrl Pts',(0.,1.15998989643835,-7.91606226215288));
#43050=CARTESIAN_POINT('Ctrl Pts',(1.5,1.15998989643835,-7.91606226215288));
#43051=CARTESIAN_POINT('Ctrl Pts',(0.,1.02258696336842,-7.93498167595306));
#43052=CARTESIAN_POINT('Ctrl Pts',(1.5,1.02258696336842,-7.93498167595306));
#43053=CARTESIAN_POINT('Ctrl Pts',(0.,0.884876701085412,-7.95151630311911));
#43054=CARTESIAN_POINT('Ctrl Pts',(1.5,0.884876701085412,-7.95151630311911));
#43055=CARTESIAN_POINT('Ctrl Pts',(0.,0.746900497168579,-7.96566117434639));
#43056=CARTESIAN_POINT('Ctrl Pts',(1.5,0.746900497168579,-7.96566117434639));
#43057=CARTESIAN_POINT('Ctrl Pts',(0.,0.608699819089495,-7.97741203829576));
#43058=CARTESIAN_POINT('Ctrl Pts',(1.5,0.608699819089495,-7.97741203829576));
#43059=CARTESIAN_POINT('Ctrl Pts',(0.,0.470316201774848,-7.98676536311966));
#43060=CARTESIAN_POINT('Ctrl Pts',(1.5,0.470316201774848,-7.98676536311966));
#43061=CARTESIAN_POINT('Ctrl Pts',(0.,0.331791235173314,-7.99371833803316));
#43062=CARTESIAN_POINT('Ctrl Pts',(1.5,0.331791235173314,-7.99371833803316));
#43063=CARTESIAN_POINT('Ctrl Pts',(0.,0.193166551724818,-7.99826887364049));
#43064=CARTESIAN_POINT('Ctrl Pts',(1.5,0.193166551724818,-7.99826887364049));
#43065=CARTESIAN_POINT('Ctrl Pts',(0.,0.0544838138324683,-8.00041560230666));
#43066=CARTESIAN_POINT('Ctrl Pts',(1.5,0.0544838138324683,-8.00041560230666));
#43067=CARTESIAN_POINT('Ctrl Pts',(0.,-0.0842152986636308,-8.0001578785741));
#43068=CARTESIAN_POINT('Ctrl Pts',(1.5,-0.0842152986636308,-8.0001578785741));
#43069=CARTESIAN_POINT('Ctrl Pts',(0.,-0.222889101011495,-7.99749577962445));
#43070=CARTESIAN_POINT('Ctrl Pts',(1.5,-0.222889101011495,-7.99749577962445));
#43071=CARTESIAN_POINT('Ctrl Pts',(0.,-0.361495916071951,-7.99243010578557));
#43072=CARTESIAN_POINT('Ctrl Pts',(1.5,-0.361495916071951,-7.99243010578557));
#43073=CARTESIAN_POINT('Ctrl Pts',(0.,-0.499994086829513,-7.98496237976419));
#43074=CARTESIAN_POINT('Ctrl Pts',(1.5,-0.499994086829513,-7.98496237976419));
#43075=CARTESIAN_POINT('Ctrl Pts',(0.,-0.638341988904545,-7.9750948459236));
#43076=CARTESIAN_POINT('Ctrl Pts',(1.5,-0.638341988904545,-7.9750948459236));
#43077=CARTESIAN_POINT('Ctrl Pts',(0.,-0.776498043067469,-7.96283046960652));
#43078=CARTESIAN_POINT('Ctrl Pts',(1.5,-0.776498043067469,-7.96283046960652));
#43079=CARTESIAN_POINT('Ctrl Pts',(0.,-0.914420727755825,-7.94817293650308));
#43080=CARTESIAN_POINT('Ctrl Pts',(1.5,-0.914420727755825,-7.94817293650308));
#43081=CARTESIAN_POINT('Ctrl Pts',(0.,-1.05206859159497,-7.93112665206354));
#43082=CARTESIAN_POINT('Ctrl Pts',(1.5,-1.05206859159497,-7.93112665206354));
#43083=CARTESIAN_POINT('Ctrl Pts',(0.,-1.18940026579597,-7.91169673965436));
#43084=CARTESIAN_POINT('Ctrl Pts',(1.5,-1.18940026579597,-7.91169673965436));
#43085=CARTESIAN_POINT('Ctrl Pts',(0.,-1.3263744765588,-7.88988903875861));
#43086=CARTESIAN_POINT('Ctrl Pts',(1.5,-1.3263744765588,-7.88988903875861));
#43087=CARTESIAN_POINT('Ctrl Pts',(0.,-1.4629500574812,-7.86571010322161));
#43088=CARTESIAN_POINT('Ctrl Pts',(1.5,-1.4629500574812,-7.86571010322161));
#43089=CARTESIAN_POINT('Ctrl Pts',(0.,-1.59908596197461,-7.83916719954087));
#43090=CARTESIAN_POINT('Ctrl Pts',(1.5,-1.59908596197461,-7.83916719954087));
#43091=CARTESIAN_POINT('Ctrl Pts',(0.,-1.73474127568722,-7.81026830520049));
#43092=CARTESIAN_POINT('Ctrl Pts',(1.5,-1.73474127568722,-7.81026830520049));
#43093=CARTESIAN_POINT('Ctrl Pts',(0.,-1.86987522869551,-7.77902210575902));
#43094=CARTESIAN_POINT('Ctrl Pts',(1.5,-1.86987522869551,-7.77902210575902));
#43095=CARTESIAN_POINT('Ctrl Pts',(0.,-2.00444720770498,-7.74543799198167));
#43096=CARTESIAN_POINT('Ctrl Pts',(1.5,-2.00444720770498,-7.74543799198167));
#43097=CARTESIAN_POINT('Ctrl Pts',(0.,-2.13841676826037,-7.70952605701667));
#43098=CARTESIAN_POINT('Ctrl Pts',(1.5,-2.13841676826037,-7.70952605701667));
#43099=CARTESIAN_POINT('Ctrl Pts',(0.,-2.27174364696663,-7.67129709361539));
#43100=CARTESIAN_POINT('Ctrl Pts',(1.5,-2.27174364696663,-7.67129709361539));
#43101=CARTESIAN_POINT('Ctrl Pts',(0.,-2.40438777372114,-7.63076259139598));
#43102=CARTESIAN_POINT('Ctrl Pts',(1.5,-2.40438777372114,-7.63076259139598));
#43103=CARTESIAN_POINT('Ctrl Pts',(0.,-2.53630928360746,-7.58793473288758));
#43104=CARTESIAN_POINT('Ctrl Pts',(1.5,-2.53630928360746,-7.58793473288758));
#43105=CARTESIAN_POINT('Ctrl Pts',(0.,-2.66746852880189,-7.54282638961755));
#43106=CARTESIAN_POINT('Ctrl Pts',(1.5,-2.66746852880189,-7.54282638961755));
#43107=CARTESIAN_POINT('Ctrl Pts',(0.,-2.79782609049359,-7.49545111824191));
#43108=CARTESIAN_POINT('Ctrl Pts',(1.5,-2.79782609049359,-7.49545111824191));
#43109=CARTESIAN_POINT('Ctrl Pts',(0.,-2.92734279081898,-7.4458231567185));
#43110=CARTESIAN_POINT('Ctrl Pts',(1.5,-2.92734279081898,-7.4458231567185));
#43111=CARTESIAN_POINT('Ctrl Pts',(0.,-3.05597970481126,-7.39395742052261));
#43112=CARTESIAN_POINT('Ctrl Pts',(1.5,-3.05597970481126,-7.39395742052261));
#43113=CARTESIAN_POINT('Ctrl Pts',(0.,-3.18369817190697,-7.33986949767589));
#43114=CARTESIAN_POINT('Ctrl Pts',(1.5,-3.18369817190697,-7.33986949767589));
#43115=CARTESIAN_POINT('Ctrl Pts',(0.,-3.31045980746918,-7.28357564381743));
#43116=CARTESIAN_POINT('Ctrl Pts',(1.5,-3.31045980746918,-7.28357564381743));
#43117=CARTESIAN_POINT('Ctrl Pts',(0.,-3.43622651432776,-7.2250927773164));
#43118=CARTESIAN_POINT('Ctrl Pts',(1.5,-3.43622651432776,-7.2250927773164));
#43119=CARTESIAN_POINT('Ctrl Pts',(0.,-3.56096049433766,-7.16443847442603));
#43120=CARTESIAN_POINT('Ctrl Pts',(1.5,-3.56096049433766,-7.16443847442603));
#43121=CARTESIAN_POINT('Ctrl Pts',(0.,-3.6846242599558,-7.10163096447882));
#43122=CARTESIAN_POINT('Ctrl Pts',(1.5,-3.6846242599558,-7.10163096447882));
#43123=CARTESIAN_POINT('Ctrl Pts',(0.,-3.80718064527425,-7.03668912393815));
#43124=CARTESIAN_POINT('Ctrl Pts',(1.5,-3.80718064527425,-7.03668912393815));
#43125=CARTESIAN_POINT('Ctrl Pts',(0.,-3.92859281707327,-6.96963247049021));
#43126=CARTESIAN_POINT('Ctrl Pts',(1.5,-3.92859281707327,-6.96963247049021));
#43127=CARTESIAN_POINT('Ctrl Pts',(0.,-4.04882428589532,-6.90048115717619));
#43128=CARTESIAN_POINT('Ctrl Pts',(1.5,-4.04882428589532,-6.90048115717619));
#43129=CARTESIAN_POINT('Ctrl Pts',(0.,-4.16783891714033,-6.82925596656376));
#43130=CARTESIAN_POINT('Ctrl Pts',(1.5,-4.16783891714033,-6.82925596656376));
#43131=CARTESIAN_POINT('Ctrl Pts',(0.,-4.28560094218327,-6.75597830495819));
#43132=CARTESIAN_POINT('Ctrl Pts',(1.5,-4.28560094218327,-6.75597830495819));
#43133=CARTESIAN_POINT('Ctrl Pts',(0.,-4.40207496885083,-6.6806701955211));
#43134=CARTESIAN_POINT('Ctrl Pts',(1.5,-4.40207496885083,-6.6806701955211));
#43135=CARTESIAN_POINT('Ctrl Pts',(0.,-4.51722599192152,-6.60335427142775));
#43136=CARTESIAN_POINT('Ctrl Pts',(1.5,-4.51722599192152,-6.60335427142775));
#43137=CARTESIAN_POINT('Ctrl Pts',(0.,-4.63101940365,-6.52405376906231));
#43138=CARTESIAN_POINT('Ctrl Pts',(1.5,-4.63101940365,-6.52405376906231));
#43139=CARTESIAN_POINT('Ctrl Pts',(0.,-4.74342100431622,-6.44279252125083));
#43140=CARTESIAN_POINT('Ctrl Pts',(1.5,-4.74342100431622,-6.44279252125083));
#43141=CARTESIAN_POINT('Ctrl Pts',(0.,-4.85439701280005,-6.35959495053137));
#43142=CARTESIAN_POINT('Ctrl Pts',(1.5,-4.85439701280005,-6.35959495053137));
#43143=CARTESIAN_POINT('Ctrl Pts',(0.,-4.96391407642278,-6.27448606139168));
#43144=CARTESIAN_POINT('Ctrl Pts',(1.5,-4.96391407642278,-6.27448606139168));
#43145=CARTESIAN_POINT('Ctrl Pts',(0.,-5.07193928081559,-6.18749143254318));
#43146=CARTESIAN_POINT('Ctrl Pts',(1.5,-5.07193928081559,-6.18749143254318));
#43147=CARTESIAN_POINT('Ctrl Pts',(0.,-5.17844015981525,-6.0986372092306));
#43148=CARTESIAN_POINT('Ctrl Pts',(1.5,-5.17844015981525,-6.0986372092306));
#43149=CARTESIAN_POINT('Ctrl Pts',(0.,-5.28338470538775,-6.00795009557728));
#43150=CARTESIAN_POINT('Ctrl Pts',(1.5,-5.28338470538775,-6.00795009557728));
#43151=CARTESIAN_POINT('Ctrl Pts',(0.,-5.38674137758061,-5.91545734696511));
#43152=CARTESIAN_POINT('Ctrl Pts',(1.5,-5.38674137758061,-5.91545734696511));
#43153=CARTESIAN_POINT('Ctrl Pts',(0.,-5.48847911365542,-5.82118676144916));
#43154=CARTESIAN_POINT('Ctrl Pts',(1.5,-5.48847911365542,-5.82118676144916));
#43155=CARTESIAN_POINT('Ctrl Pts',(0.,-5.58856733725029,-5.72516667120635));
#43156=CARTESIAN_POINT('Ctrl Pts',(1.5,-5.58856733725029,-5.72516667120635));
#43157=CARTESIAN_POINT('Ctrl Pts',(0.,-5.68697596757266,-5.6274259340173));
#43158=CARTESIAN_POINT('Ctrl Pts',(1.5,-5.68697596757266,-5.6274259340173));
#43159=CARTESIAN_POINT('Ctrl Pts',(0.,-5.783675428623,-5.52799392478112));
#43160=CARTESIAN_POINT('Ctrl Pts',(1.5,-5.783675428623,-5.52799392478112));
#43161=CARTESIAN_POINT('Ctrl Pts',(0.,-5.87863665845019,-5.42690052706247));
#43162=CARTESIAN_POINT('Ctrl Pts',(1.5,-5.87863665845019,-5.42690052706247));
#43163=CARTESIAN_POINT('Ctrl Pts',(0.,-5.97183111750645,-5.32417612374785));
#43164=CARTESIAN_POINT('Ctrl Pts',(1.5,-5.97183111750645,-5.32417612374785));
#43165=CARTESIAN_POINT('Ctrl Pts',(0.,-6.06323079703504,-5.21985158773308));
#43166=CARTESIAN_POINT('Ctrl Pts',(1.5,-6.06323079703504,-5.21985158773308));
#43167=CARTESIAN_POINT('Ctrl Pts',(0.,-6.15280822749109,-5.11395827264137));
#43168=CARTESIAN_POINT('Ctrl Pts',(1.5,-6.15280822749109,-5.11395827264137));
#43169=CARTESIAN_POINT('Ctrl Pts',(0.,-6.2405364869961,-5.0065280035714));
#43170=CARTESIAN_POINT('Ctrl Pts',(1.5,-6.2405364869961,-5.0065280035714));
#43171=CARTESIAN_POINT('Ctrl Pts',(0.,-6.32638920982662,-4.89759306787482));
#43172=CARTESIAN_POINT('Ctrl Pts',(1.5,-6.32638920982662,-4.89759306787482));
#43173=CARTESIAN_POINT('Ctrl Pts',(0.,-6.41034059392906,-4.78718620512425));
#43174=CARTESIAN_POINT('Ctrl Pts',(1.5,-6.41034059392906,-4.78718620512425));
#43175=CARTESIAN_POINT('Ctrl Pts',(0.,-6.49236540846972,-4.67534059710961));
#43176=CARTESIAN_POINT('Ctrl Pts',(1.5,-6.49236540846972,-4.67534059710961));
#43177=CARTESIAN_POINT('Ctrl Pts',(0.,-6.57243900142041,-4.56208985786201));
#43178=CARTESIAN_POINT('Ctrl Pts',(1.5,-6.57243900142041,-4.56208985786201));
#43179=CARTESIAN_POINT('Ctrl Pts',(0.,-6.65053730718027,-4.44746802370464));
#43180=CARTESIAN_POINT('Ctrl Pts',(1.5,-6.65053730718027,-4.44746802370464));
#43181=CARTESIAN_POINT('Ctrl Pts',(0.,-6.72663685423419,-4.33150954333007));
#43182=CARTESIAN_POINT('Ctrl Pts',(1.5,-6.72663685423419,-4.33150954333007));
#43183=CARTESIAN_POINT('Ctrl Pts',(0.,-6.80071477177081,-4.21424926715533));
#43184=CARTESIAN_POINT('Ctrl Pts',(1.5,-6.80071477177081,-4.21424926715533));
#43185=CARTESIAN_POINT('Ctrl Pts',(0.,-6.87274879633804,-4.09572243670215));
#43186=CARTESIAN_POINT('Ctrl Pts',(1.5,-6.87274879633804,-4.09572243670215));
#43187=CARTESIAN_POINT('Ctrl Pts',(0.,-6.94271727853662,-3.97596467400157));
#43188=CARTESIAN_POINT('Ctrl Pts',(1.5,-6.94271727853662,-3.97596467400157));
#43189=CARTESIAN_POINT('Ctrl Pts',(0.,-7.01059918975196,-3.85501197102232));
#43190=CARTESIAN_POINT('Ctrl Pts',(1.5,-7.01059918975196,-3.85501197102232));
#43191=CARTESIAN_POINT('Ctrl Pts',(0.,-7.07637412892475,-3.73290067912243));
#43192=CARTESIAN_POINT('Ctrl Pts',(1.5,-7.07637412892475,-3.73290067912243));
#43193=CARTESIAN_POINT('Ctrl Pts',(0.,-7.14002232822272,-3.60966749787132));
#43194=CARTESIAN_POINT('Ctrl Pts',(1.5,-7.14002232822272,-3.60966749787132));
#43195=CARTESIAN_POINT('Ctrl Pts',(0.,-7.20152465875188,-3.48534946389366));
#43196=CARTESIAN_POINT('Ctrl Pts',(1.5,-7.20152465875188,-3.48534946389366));
#43197=CARTESIAN_POINT('Ctrl Pts',(0.,-7.26086263630753,-3.3599839397343));
#43198=CARTESIAN_POINT('Ctrl Pts',(1.5,-7.26086263630753,-3.3599839397343));
#43199=CARTESIAN_POINT('Ctrl Pts',(0.,-7.31801842716562,-3.23360860274355));
#43200=CARTESIAN_POINT('Ctrl Pts',(1.5,-7.31801842716562,-3.23360860274355));
#43201=CARTESIAN_POINT('Ctrl Pts',(0.,-7.37297485391472,-3.1062614339821));
#43202=CARTESIAN_POINT('Ctrl Pts',(1.5,-7.37297485391472,-3.1062614339821));
#43203=CARTESIAN_POINT('Ctrl Pts',(0.,-7.42571540013862,-2.97798070659427));
#43204=CARTESIAN_POINT('Ctrl Pts',(1.5,-7.42571540013862,-2.97798070659427));
#43205=CARTESIAN_POINT('Ctrl Pts',(0.,-7.47622421514032,-2.84880497419933));
#43206=CARTESIAN_POINT('Ctrl Pts',(1.5,-7.47622421514032,-2.84880497419933));
#43207=CARTESIAN_POINT('Ctrl Pts',(0.,-7.52448611870752,-2.71877305930032));
#43208=CARTESIAN_POINT('Ctrl Pts',(1.5,-7.52448611870752,-2.71877305930032));
#43209=CARTESIAN_POINT('Ctrl Pts',(0.,-7.57048660592005,-2.58792404170972));
#43210=CARTESIAN_POINT('Ctrl Pts',(1.5,-7.57048660592005,-2.58792404170972));
#43211=CARTESIAN_POINT('Ctrl Pts',(0.,-7.61421185199946,-2.45629724699105));
#43212=CARTESIAN_POINT('Ctrl Pts',(1.5,-7.61421185199946,-2.45629724699105));
#43213=CARTESIAN_POINT('Ctrl Pts',(0.,-7.65564871596749,-2.32393223447027));
#43214=CARTESIAN_POINT('Ctrl Pts',(1.5,-7.65564871596749,-2.32393223447027));
#43215=CARTESIAN_POINT('Ctrl Pts',(0.,-7.69478474434726,-2.19086878526178));
#43216=CARTESIAN_POINT('Ctrl Pts',(1.5,-7.69478474434726,-2.19086878526178));
#43217=CARTESIAN_POINT('Ctrl Pts',(0.,-7.73160817490736,-2.05714689030825));
#43218=CARTESIAN_POINT('Ctrl Pts',(1.5,-7.73160817490736,-2.05714689030825));
#43219=CARTESIAN_POINT('Ctrl Pts',(0.,-7.76610794044926,-1.92280673843347));
#43220=CARTESIAN_POINT('Ctrl Pts',(1.5,-7.76610794044926,-1.92280673843347));
#43221=CARTESIAN_POINT('Ctrl Pts',(0.,-7.79827367263786,-1.78788870440769));
#43222=CARTESIAN_POINT('Ctrl Pts',(1.5,-7.79827367263786,-1.78788870440769));
#43223=CARTESIAN_POINT('Ctrl Pts',(0.,-7.82809570460851,-1.65243333668723));
#43224=CARTESIAN_POINT('Ctrl Pts',(1.5,-7.82809570460851,-1.65243333668723));
#43225=CARTESIAN_POINT('Ctrl Pts',(0.,-7.8555650736176,-1.516481345165));
#43226=CARTESIAN_POINT('Ctrl Pts',(1.5,-7.8555650736176,-1.516481345165));
#43227=CARTESIAN_POINT('Ctrl Pts',(0.,-7.8806735237373,-1.38007358893105));
#43228=CARTESIAN_POINT('Ctrl Pts',(1.5,-7.8806735237373,-1.38007358893105));
#43229=CARTESIAN_POINT('Ctrl Pts',(0.,-7.90341350859433,-1.24325106404244));
#43230=CARTESIAN_POINT('Ctrl Pts',(1.5,-7.90341350859433,-1.24325106404244));
#43231=CARTESIAN_POINT('Ctrl Pts',(0.,-7.92377819415291,-1.1060548913017));
#43232=CARTESIAN_POINT('Ctrl Pts',(1.5,-7.92377819415291,-1.1060548913017));
#43233=CARTESIAN_POINT('Ctrl Pts',(0.,-7.94176146025056,-0.968526303816797));
#43234=CARTESIAN_POINT('Ctrl Pts',(1.5,-7.94176146025056,-0.968526303816797));
#43235=CARTESIAN_POINT('Ctrl Pts',(0.,-7.9573579021783,-0.830706634568147));
#43236=CARTESIAN_POINT('Ctrl Pts',(1.5,-7.9573579021783,-0.830706634568147));
#43237=CARTESIAN_POINT('Ctrl Pts',(0.,-7.97056283230563,-0.692637303981898));
#43238=CARTESIAN_POINT('Ctrl Pts',(1.5,-7.97056283230563,-0.692637303981898));
#43239=CARTESIAN_POINT('Ctrl Pts',(0.,-7.98137228175028,-0.55435980750864));
#43240=CARTESIAN_POINT('Ctrl Pts',(1.5,-7.98137228175028,-0.55435980750864));
#43241=CARTESIAN_POINT('Ctrl Pts',(0.,-7.98978300209272,-0.415915703206775));
#43242=CARTESIAN_POINT('Ctrl Pts',(1.5,-7.98978300209272,-0.415915703206775));
#43243=CARTESIAN_POINT('Ctrl Pts',(0.,-7.99579246582898,-0.277346599216242));
#43244=CARTESIAN_POINT('Ctrl Pts',(1.5,-7.99579246582898,-0.277346599216242));
#43245=CARTESIAN_POINT('Ctrl Pts',(0.,-7.99939886686876,-0.138694141235355));
#43246=CARTESIAN_POINT('Ctrl Pts',(1.5,-7.99939886686876,-0.138694141235355));
#43247=CARTESIAN_POINT('Ctrl Pts',(0.,-8.00060112107831,-7.07794283252849E-14));
#43248=CARTESIAN_POINT('Ctrl Pts',(1.5,-8.00060112107831,-7.07794283252849E-14));
#43249=CARTESIAN_POINT('Ctrl Pts',(0.,-7.9993988668687,0.138694141235229));
#43250=CARTESIAN_POINT('Ctrl Pts',(1.5,-7.9993988668687,0.138694141235229));
#43251=CARTESIAN_POINT('Ctrl Pts',(0.,-7.99579246582889,0.277346599216146));
#43252=CARTESIAN_POINT('Ctrl Pts',(1.5,-7.99579246582889,0.277346599216146));
#43253=CARTESIAN_POINT('Ctrl Pts',(0.,-7.98978300209264,0.415915703206705));
#43254=CARTESIAN_POINT('Ctrl Pts',(1.5,-7.98978300209264,0.415915703206705));
#43255=CARTESIAN_POINT('Ctrl Pts',(0.,-7.98137228175027,0.554359807508556));
#43256=CARTESIAN_POINT('Ctrl Pts',(1.5,-7.98137228175027,0.554359807508556));
#43257=CARTESIAN_POINT('Ctrl Pts',(0.,-7.97056283230564,0.692637303981767));
#43258=CARTESIAN_POINT('Ctrl Pts',(1.5,-7.97056283230564,0.692637303981767));
#43259=CARTESIAN_POINT('Ctrl Pts',(0.,-7.95735790217834,0.830706634567969));
#43260=CARTESIAN_POINT('Ctrl Pts',(1.5,-7.95735790217834,0.830706634567969));
#43261=CARTESIAN_POINT('Ctrl Pts',(0.,-7.94176146025064,0.968526303816614));
#43262=CARTESIAN_POINT('Ctrl Pts',(1.5,-7.94176146025064,0.968526303816614));
#43263=CARTESIAN_POINT('Ctrl Pts',(0.,-7.92377819415303,1.10605489130155));
#43264=CARTESIAN_POINT('Ctrl Pts',(1.5,-7.92377819415303,1.10605489130155));
#43265=CARTESIAN_POINT('Ctrl Pts',(0.,-7.90341350859442,1.24325106404233));
#43266=CARTESIAN_POINT('Ctrl Pts',(1.5,-7.90341350859442,1.24325106404233));
#43267=CARTESIAN_POINT('Ctrl Pts',(0.,-7.88067352373733,1.38007358893094));
#43268=CARTESIAN_POINT('Ctrl Pts',(1.5,-7.88067352373733,1.38007358893094));
#43269=CARTESIAN_POINT('Ctrl Pts',(0.,-7.85556507361753,1.51648134516485));
#43270=CARTESIAN_POINT('Ctrl Pts',(1.5,-7.85556507361753,1.51648134516485));
#43271=CARTESIAN_POINT('Ctrl Pts',(0.,-7.8280957046084,1.65243333668702));
#43272=CARTESIAN_POINT('Ctrl Pts',(1.5,-7.8280957046084,1.65243333668702));
#43273=CARTESIAN_POINT('Ctrl Pts',(0.,-7.79827367263774,1.78788870440746));
#43274=CARTESIAN_POINT('Ctrl Pts',(1.5,-7.79827367263774,1.78788870440746));
#43275=CARTESIAN_POINT('Ctrl Pts',(0.,-7.76610794044919,1.92280673843328));
#43276=CARTESIAN_POINT('Ctrl Pts',(1.5,-7.76610794044919,1.92280673843328));
#43277=CARTESIAN_POINT('Ctrl Pts',(0.,-7.73160817490739,2.05714689030813));
#43278=CARTESIAN_POINT('Ctrl Pts',(1.5,-7.73160817490739,2.05714689030813));
#43279=CARTESIAN_POINT('Ctrl Pts',(0.,-7.69478474434738,2.19086878526173));
#43280=CARTESIAN_POINT('Ctrl Pts',(1.5,-7.69478474434738,2.19086878526173));
#43281=CARTESIAN_POINT('Ctrl Pts',(0.,-7.65564871596768,2.32393223447026));
#43282=CARTESIAN_POINT('Ctrl Pts',(1.5,-7.65564871596768,2.32393223447026));
#43283=CARTESIAN_POINT('Ctrl Pts',(0.,-7.61421185199964,2.45629724699104));
#43284=CARTESIAN_POINT('Ctrl Pts',(1.5,-7.61421185199964,2.45629724699104));
#43285=CARTESIAN_POINT('Ctrl Pts',(0.,-7.57048660592016,2.58792404170968));
#43286=CARTESIAN_POINT('Ctrl Pts',(1.5,-7.57048660592016,2.58792404170968));
#43287=CARTESIAN_POINT('Ctrl Pts',(0.,-7.52448611870755,2.71877305930021));
#43288=CARTESIAN_POINT('Ctrl Pts',(1.5,-7.52448611870755,2.71877305930021));
#43289=CARTESIAN_POINT('Ctrl Pts',(0.,-7.47622421514032,2.84880497419911));
#43290=CARTESIAN_POINT('Ctrl Pts',(1.5,-7.47622421514032,2.84880497419911));
#43291=CARTESIAN_POINT('Ctrl Pts',(0.,-7.42571540013867,2.97798070659398));
#43292=CARTESIAN_POINT('Ctrl Pts',(1.5,-7.42571540013867,2.97798070659398));
#43293=CARTESIAN_POINT('Ctrl Pts',(0.,-7.37297485391485,3.10626143398182));
#43294=CARTESIAN_POINT('Ctrl Pts',(1.5,-7.37297485391485,3.10626143398182));
#43295=CARTESIAN_POINT('Ctrl Pts',(0.,-7.31801842716578,3.23360860274336));
#43296=CARTESIAN_POINT('Ctrl Pts',(1.5,-7.31801842716578,3.23360860274336));
#43297=CARTESIAN_POINT('Ctrl Pts',(0.,-7.2608626363076,3.35998393973421));
#43298=CARTESIAN_POINT('Ctrl Pts',(1.5,-7.2608626363076,3.35998393973421));
#43299=CARTESIAN_POINT('Ctrl Pts',(0.,-7.20152465875178,3.48534946389357));
#43300=CARTESIAN_POINT('Ctrl Pts',(1.5,-7.20152465875178,3.48534946389357));
#43301=CARTESIAN_POINT('Ctrl Pts',(0.,-7.14002232822245,3.60966749787115));
#43302=CARTESIAN_POINT('Ctrl Pts',(1.5,-7.14002232822245,3.60966749787115));
#43303=CARTESIAN_POINT('Ctrl Pts',(0.,-7.07637412892443,3.7329006791222));
#43304=CARTESIAN_POINT('Ctrl Pts',(1.5,-7.07637412892443,3.7329006791222));
#43305=CARTESIAN_POINT('Ctrl Pts',(0.,-7.01059918975178,3.8550119710221));
#43306=CARTESIAN_POINT('Ctrl Pts',(1.5,-7.01059918975178,3.8550119710221));
#43307=CARTESIAN_POINT('Ctrl Pts',(0.,-6.94271727853668,3.97596467400145));
#43308=CARTESIAN_POINT('Ctrl Pts',(1.5,-6.94271727853668,3.97596467400145));
#43309=CARTESIAN_POINT('Ctrl Pts',(0.,-6.87274879633835,4.09572243670218));
#43310=CARTESIAN_POINT('Ctrl Pts',(1.5,-6.87274879633835,4.09572243670218));
#43311=CARTESIAN_POINT('Ctrl Pts',(0.,-6.80071477177124,4.21424926715544));
#43312=CARTESIAN_POINT('Ctrl Pts',(1.5,-6.80071477177124,4.21424926715544));
#43313=CARTESIAN_POINT('Ctrl Pts',(0.,-6.7266368542346,4.33150954333015));
#43314=CARTESIAN_POINT('Ctrl Pts',(1.5,-6.7266368542346,4.33150954333015));
#43315=CARTESIAN_POINT('Ctrl Pts',(0.,-6.65053730718051,4.44746802370462));
#43316=CARTESIAN_POINT('Ctrl Pts',(1.5,-6.65053730718051,4.44746802370462));
#43317=CARTESIAN_POINT('Ctrl Pts',(0.,-6.57243900142046,4.56208985786189));
#43318=CARTESIAN_POINT('Ctrl Pts',(1.5,-6.57243900142046,4.56208985786189));
#43319=CARTESIAN_POINT('Ctrl Pts',(0.,-6.49236540846965,4.67534059710945));
#43320=CARTESIAN_POINT('Ctrl Pts',(1.5,-6.49236540846965,4.67534059710945));
#43321=CARTESIAN_POINT('Ctrl Pts',(0.,-6.41034059392897,4.78718620512409));
#43322=CARTESIAN_POINT('Ctrl Pts',(1.5,-6.41034059392897,4.78718620512409));
#43323=CARTESIAN_POINT('Ctrl Pts',(0.,-6.32638920982654,4.89759306787468));
#43324=CARTESIAN_POINT('Ctrl Pts',(1.5,-6.32638920982654,4.89759306787468));
#43325=CARTESIAN_POINT('Ctrl Pts',(0.,-6.2405364869961,5.0065280035713));
#43326=CARTESIAN_POINT('Ctrl Pts',(1.5,-6.2405364869961,5.0065280035713));
#43327=CARTESIAN_POINT('Ctrl Pts',(0.,-6.15280822749117,5.11395827264129));
#43328=CARTESIAN_POINT('Ctrl Pts',(1.5,-6.15280822749117,5.11395827264129));
#43329=CARTESIAN_POINT('Ctrl Pts',(0.,-6.0632307970352,5.21985158773299));
#43330=CARTESIAN_POINT('Ctrl Pts',(1.5,-6.0632307970352,5.21985158773299));
#43331=CARTESIAN_POINT('Ctrl Pts',(0.,-5.97183111750664,5.32417612374773));
#43332=CARTESIAN_POINT('Ctrl Pts',(1.5,-5.97183111750664,5.32417612374773));
#43333=CARTESIAN_POINT('Ctrl Pts',(0.,-5.87863665845037,5.42690052706231));
#43334=CARTESIAN_POINT('Ctrl Pts',(1.5,-5.87863665845037,5.42690052706231));
#43335=CARTESIAN_POINT('Ctrl Pts',(0.,-5.78367542862314,5.52799392478097));
#43336=CARTESIAN_POINT('Ctrl Pts',(1.5,-5.78367542862314,5.52799392478097));
#43337=CARTESIAN_POINT('Ctrl Pts',(0.,-5.68697596757273,5.62742593401721));
#43338=CARTESIAN_POINT('Ctrl Pts',(1.5,-5.68697596757273,5.62742593401721));
#43339=CARTESIAN_POINT('Ctrl Pts',(0.,-5.58856733725033,5.72516667120635));
#43340=CARTESIAN_POINT('Ctrl Pts',(1.5,-5.58856733725033,5.72516667120635));
#43341=CARTESIAN_POINT('Ctrl Pts',(0.,-5.48847911365546,5.82118676144923));
#43342=CARTESIAN_POINT('Ctrl Pts',(1.5,-5.48847911365546,5.82118676144923));
#43343=CARTESIAN_POINT('Ctrl Pts',(0.,-5.38674137758068,5.91545734696517));
#43344=CARTESIAN_POINT('Ctrl Pts',(1.5,-5.38674137758068,5.91545734696517));
#43345=CARTESIAN_POINT('Ctrl Pts',(0.,-5.28338470538786,6.0079500955773));
#43346=CARTESIAN_POINT('Ctrl Pts',(1.5,-5.28338470538786,6.0079500955773));
#43347=CARTESIAN_POINT('Ctrl Pts',(0.,-5.17844015981534,6.09863720923052));
#43348=CARTESIAN_POINT('Ctrl Pts',(1.5,-5.17844015981534,6.09863720923052));
#43349=CARTESIAN_POINT('Ctrl Pts',(0.,-5.07193928081565,6.18749143254302));
#43350=CARTESIAN_POINT('Ctrl Pts',(1.5,-5.07193928081565,6.18749143254302));
#43351=CARTESIAN_POINT('Ctrl Pts',(0.,-4.96391407642283,6.27448606139153));
#43352=CARTESIAN_POINT('Ctrl Pts',(1.5,-4.96391407642283,6.27448606139153));
#43353=CARTESIAN_POINT('Ctrl Pts',(0.,-4.85439701280011,6.35959495053125));
#43354=CARTESIAN_POINT('Ctrl Pts',(1.5,-4.85439701280011,6.35959495053125));
#43355=CARTESIAN_POINT('Ctrl Pts',(0.,-4.74342100431631,6.44279252125077));
#43356=CARTESIAN_POINT('Ctrl Pts',(1.5,-4.74342100431631,6.44279252125077));
#43357=CARTESIAN_POINT('Ctrl Pts',(0.,-4.63101940365009,6.52405376906226));
#43358=CARTESIAN_POINT('Ctrl Pts',(1.5,-4.63101940365009,6.52405376906226));
#43359=CARTESIAN_POINT('Ctrl Pts',(0.,-4.51722599192163,6.60335427142766));
#43360=CARTESIAN_POINT('Ctrl Pts',(1.5,-4.51722599192163,6.60335427142766));
#43361=CARTESIAN_POINT('Ctrl Pts',(0.,-4.40207496885094,6.68067019552094));
#43362=CARTESIAN_POINT('Ctrl Pts',(1.5,-4.40207496885094,6.68067019552094));
#43363=CARTESIAN_POINT('Ctrl Pts',(0.,-4.28560094218339,6.75597830495801));
#43364=CARTESIAN_POINT('Ctrl Pts',(1.5,-4.28560094218339,6.75597830495801));
#43365=CARTESIAN_POINT('Ctrl Pts',(0.,-4.16783891714045,6.82925596656362));
#43366=CARTESIAN_POINT('Ctrl Pts',(1.5,-4.16783891714045,6.82925596656362));
#43367=CARTESIAN_POINT('Ctrl Pts',(0.,-4.04882428589543,6.90048115717614));
#43368=CARTESIAN_POINT('Ctrl Pts',(1.5,-4.04882428589543,6.90048115717614));
#43369=CARTESIAN_POINT('Ctrl Pts',(0.,-3.92859281707335,6.96963247049021));
#43370=CARTESIAN_POINT('Ctrl Pts',(1.5,-3.92859281707335,6.96963247049021));
#43371=CARTESIAN_POINT('Ctrl Pts',(0.,-3.80718064527426,7.03668912393813));
#43372=CARTESIAN_POINT('Ctrl Pts',(1.5,-3.80718064527426,7.03668912393813));
#43373=CARTESIAN_POINT('Ctrl Pts',(0.,-3.68462425995581,7.10163096447878));
#43374=CARTESIAN_POINT('Ctrl Pts',(1.5,-3.68462425995581,7.10163096447878));
#43375=CARTESIAN_POINT('Ctrl Pts',(0.,-3.56096049433769,7.16443847442598));
#43376=CARTESIAN_POINT('Ctrl Pts',(1.5,-3.56096049433769,7.16443847442598));
#43377=CARTESIAN_POINT('Ctrl Pts',(0.,-3.43622651432787,7.22509277731633));
#43378=CARTESIAN_POINT('Ctrl Pts',(1.5,-3.43622651432787,7.22509277731633));
#43379=CARTESIAN_POINT('Ctrl Pts',(0.,-3.31045980746936,7.28357564381742));
#43380=CARTESIAN_POINT('Ctrl Pts',(1.5,-3.31045980746936,7.28357564381742));
#43381=CARTESIAN_POINT('Ctrl Pts',(0.,-3.18369817190718,7.33986949767594));
#43382=CARTESIAN_POINT('Ctrl Pts',(1.5,-3.18369817190718,7.33986949767594));
#43383=CARTESIAN_POINT('Ctrl Pts',(0.,-3.05597970481146,7.39395742052271));
#43384=CARTESIAN_POINT('Ctrl Pts',(1.5,-3.05597970481146,7.39395742052271));
#43385=CARTESIAN_POINT('Ctrl Pts',(0.,-2.92734279081915,7.44582315671858));
#43386=CARTESIAN_POINT('Ctrl Pts',(1.5,-2.92734279081915,7.44582315671858));
#43387=CARTESIAN_POINT('Ctrl Pts',(0.,-2.7978260904937,7.49545111824188));
#43388=CARTESIAN_POINT('Ctrl Pts',(1.5,-2.7978260904937,7.49545111824188));
#43389=CARTESIAN_POINT('Ctrl Pts',(0.,-2.66746852880196,7.54282638961738));
#43390=CARTESIAN_POINT('Ctrl Pts',(1.5,-2.66746852880196,7.54282638961738));
#43391=CARTESIAN_POINT('Ctrl Pts',(0.,-2.53630928360749,7.58793473288732));
#43392=CARTESIAN_POINT('Ctrl Pts',(1.5,-2.53630928360749,7.58793473288732));
#43393=CARTESIAN_POINT('Ctrl Pts',(0.,-2.40438777372116,7.63076259139572));
#43394=CARTESIAN_POINT('Ctrl Pts',(1.5,-2.40438777372116,7.63076259139572));
#43395=CARTESIAN_POINT('Ctrl Pts',(0.,-2.27174364696667,7.6712970936152));
#43396=CARTESIAN_POINT('Ctrl Pts',(1.5,-2.27174364696667,7.6712970936152));
#43397=CARTESIAN_POINT('Ctrl Pts',(0.,-2.13841676826048,7.70952605701664));
#43398=CARTESIAN_POINT('Ctrl Pts',(1.5,-2.13841676826048,7.70952605701664));
#43399=CARTESIAN_POINT('Ctrl Pts',(0.,-2.00444720770517,7.7454379919818));
#43400=CARTESIAN_POINT('Ctrl Pts',(1.5,-2.00444720770517,7.7454379919818));
#43401=CARTESIAN_POINT('Ctrl Pts',(0.,-1.86987522869577,7.77902210575933));
#43402=CARTESIAN_POINT('Ctrl Pts',(1.5,-1.86987522869577,7.77902210575933));
#43403=CARTESIAN_POINT('Ctrl Pts',(0.,-1.73474127568748,7.81026830520089));
#43404=CARTESIAN_POINT('Ctrl Pts',(1.5,-1.73474127568748,7.81026830520089));
#43405=CARTESIAN_POINT('Ctrl Pts',(0.,-1.59908596197483,7.83916719954116));
#43406=CARTESIAN_POINT('Ctrl Pts',(1.5,-1.59908596197483,7.83916719954116));
#43407=CARTESIAN_POINT('Ctrl Pts',(0.,-1.46295005748132,7.86571010322159));
#43408=CARTESIAN_POINT('Ctrl Pts',(1.5,-1.46295005748132,7.86571010322159));
#43409=CARTESIAN_POINT('Ctrl Pts',(0.,-1.32637447655881,7.88988903875827));
#43410=CARTESIAN_POINT('Ctrl Pts',(1.5,-1.32637447655881,7.88988903875827));
#43411=CARTESIAN_POINT('Ctrl Pts',(0.,-1.18940026579592,7.91169673965388));
#43412=CARTESIAN_POINT('Ctrl Pts',(1.5,-1.18940026579592,7.91169673965388));
#43413=CARTESIAN_POINT('Ctrl Pts',(0.,-1.0520685915949,7.93112665206312));
#43414=CARTESIAN_POINT('Ctrl Pts',(1.5,-1.0520685915949,7.93112665206312));
#43415=CARTESIAN_POINT('Ctrl Pts',(0.,-0.914420727755818,7.94817293650282));
#43416=CARTESIAN_POINT('Ctrl Pts',(1.5,-0.914420727755818,7.94817293650282));
#43417=CARTESIAN_POINT('Ctrl Pts',(0.,-0.776498043067579,7.96283046960651));
#43418=CARTESIAN_POINT('Ctrl Pts',(1.5,-0.776498043067579,7.96283046960651));
#43419=CARTESIAN_POINT('Ctrl Pts',(0.,-0.6383419889048,7.97509484592382));
#43420=CARTESIAN_POINT('Ctrl Pts',(1.5,-0.6383419889048,7.97509484592382));
#43421=CARTESIAN_POINT('Ctrl Pts',(0.,-0.49999408682987,7.98496237976457));
#43422=CARTESIAN_POINT('Ctrl Pts',(1.5,-0.49999408682987,7.98496237976457));
#43423=CARTESIAN_POINT('Ctrl Pts',(0.,-0.361495916072309,7.99243010578594));
#43424=CARTESIAN_POINT('Ctrl Pts',(1.5,-0.361495916072309,7.99243010578594));
#43425=CARTESIAN_POINT('Ctrl Pts',(0.,-0.222889101011755,7.99749577962464));
#43426=CARTESIAN_POINT('Ctrl Pts',(1.5,-0.222889101011755,7.99749577962464));
#43427=CARTESIAN_POINT('Ctrl Pts',(0.,-0.0842152986637398,8.00015787857408));
#43428=CARTESIAN_POINT('Ctrl Pts',(1.5,-0.0842152986637398,8.00015787857408));
#43429=CARTESIAN_POINT('Ctrl Pts',(0.,0.0544838138324916,8.0004156023065));
#43430=CARTESIAN_POINT('Ctrl Pts',(1.5,0.0544838138324916,8.0004156023065));
#43431=CARTESIAN_POINT('Ctrl Pts',(0.,0.19316655172488,7.99826887364025));
#43432=CARTESIAN_POINT('Ctrl Pts',(1.5,0.19316655172488,7.99826887364025));
#43433=CARTESIAN_POINT('Ctrl Pts',(0.,0.331791235173336,7.99371833803291));
#43434=CARTESIAN_POINT('Ctrl Pts',(1.5,0.331791235173336,7.99371833803291));
#43435=CARTESIAN_POINT('Ctrl Pts',(0.,0.470316201774787,7.98676536311949));
#43436=CARTESIAN_POINT('Ctrl Pts',(1.5,0.470316201774787,7.98676536311949));
#43437=CARTESIAN_POINT('Ctrl Pts',(0.,0.608699819089367,7.97741203829577));
#43438=CARTESIAN_POINT('Ctrl Pts',(1.5,0.608699819089367,7.97741203829577));
#43439=CARTESIAN_POINT('Ctrl Pts',(0.,0.746900497168441,7.96566117434659));
#43440=CARTESIAN_POINT('Ctrl Pts',(1.5,0.746900497168441,7.96566117434659));
#43441=CARTESIAN_POINT('Ctrl Pts',(0.,0.884876701085331,7.95151630311944));
#43442=CARTESIAN_POINT('Ctrl Pts',(1.5,0.884876701085331,7.95151630311944));
#43443=CARTESIAN_POINT('Ctrl Pts',(0.,1.02258696336839,7.9349816759534));
#43444=CARTESIAN_POINT('Ctrl Pts',(1.5,1.02258696336839,7.9349816759534));
#43445=CARTESIAN_POINT('Ctrl Pts',(0.,1.15998989643833,7.9160622621531));
#43446=CARTESIAN_POINT('Ctrl Pts',(1.5,1.15998989643833,7.9160622621531));
#43447=CARTESIAN_POINT('Ctrl Pts',(0.,1.2970442050506,7.89476374750747));
#43448=CARTESIAN_POINT('Ctrl Pts',(1.5,1.2970442050506,7.89476374750747));
#43449=CARTESIAN_POINT('Ctrl Pts',(0.,1.43370869874345,7.87109253285326));
#43450=CARTESIAN_POINT('Ctrl Pts',(1.5,1.43370869874345,7.87109253285326));
#43451=CARTESIAN_POINT('Ctrl Pts',(0.,1.56994230429259,7.84505573268319));
#43452=CARTESIAN_POINT('Ctrl Pts',(1.5,1.56994230429259,7.84505573268319));
#43453=CARTESIAN_POINT('Ctrl Pts',(0.,1.70570407796333,7.81666117246187));
#43454=CARTESIAN_POINT('Ctrl Pts',(1.5,1.70570407796333,7.81666117246187));
#43455=CARTESIAN_POINT('Ctrl Pts',(0.,1.84095321777081,7.78591738598617));
#43456=CARTESIAN_POINT('Ctrl Pts',(1.5,1.84095321777081,7.78591738598617));
#43457=CARTESIAN_POINT('Ctrl Pts',(0.,1.97564907574906,7.75283361278995));
#43458=CARTESIAN_POINT('Ctrl Pts',(1.5,1.97564907574906,7.75283361278995));
#43459=CARTESIAN_POINT('Ctrl Pts',(0.,2.10975117022968,7.71741979559267));
#43460=CARTESIAN_POINT('Ctrl Pts',(1.5,2.10975117022968,7.71741979559267));
#43461=CARTESIAN_POINT('Ctrl Pts',(0.,2.24321919813091,7.67968657779199));
#43462=CARTESIAN_POINT('Ctrl Pts',(1.5,2.24321919813091,7.67968657779199));
#43463=CARTESIAN_POINT('Ctrl Pts',(0.,2.37601304692748,7.63964529982795));
#43464=CARTESIAN_POINT('Ctrl Pts',(1.5,2.37601304692748,7.63964529982795));
#43465=CARTESIAN_POINT('Ctrl Pts',(0.,2.50809280663236,7.59730799559073));
#43466=CARTESIAN_POINT('Ctrl Pts',(1.5,2.50809280663236,7.59730799559073));
#43467=CARTESIAN_POINT('Ctrl Pts',(0.,2.63941878179114,7.55268738887154));
#43468=CARTESIAN_POINT('Ctrl Pts',(1.5,2.63941878179114,7.55268738887154));
#43469=CARTESIAN_POINT('Ctrl Pts',(0.,2.76995150348982,7.50579688985671));
#43470=CARTESIAN_POINT('Ctrl Pts',(1.5,2.76995150348982,7.50579688985671));
#43471=CARTESIAN_POINT('Ctrl Pts',(0.,2.89965174137675,7.45665059166464));
#43472=CARTESIAN_POINT('Ctrl Pts',(1.5,2.89965174137675,7.45665059166464));
#43473=CARTESIAN_POINT('Ctrl Pts',(0.,3.02848051528187,7.40526326545791));
#43474=CARTESIAN_POINT('Ctrl Pts',(1.5,3.02848051528187,7.40526326545791));
#43475=CARTESIAN_POINT('Ctrl Pts',(0.,3.15639910685162,7.35165035559758));
#43476=CARTESIAN_POINT('Ctrl Pts',(1.5,3.15639910685162,7.35165035559758));
#43477=CARTESIAN_POINT('Ctrl Pts',(0.,3.28336907120013,7.29582797483965));
#43478=CARTESIAN_POINT('Ctrl Pts',(1.5,3.28336907120013,7.29582797483965));
#43479=CARTESIAN_POINT('Ctrl Pts',(0.,3.4093522485776,7.23781289957331));
#43480=CARTESIAN_POINT('Ctrl Pts',(1.5,3.4093522485776,7.23781289957331));
#43481=CARTESIAN_POINT('Ctrl Pts',(0.,3.5343107760563,7.17762256510045));
#43482=CARTESIAN_POINT('Ctrl Pts',(1.5,3.5343107760563,7.17762256510045));
#43483=CARTESIAN_POINT('Ctrl Pts',(0.,3.65820709866192,7.1152750602933));
#43484=CARTESIAN_POINT('Ctrl Pts',(1.5,3.65820709866192,7.1152750602933));
#43485=CARTESIAN_POINT('Ctrl Pts',(0.,3.78100398052407,7.05078912229265));
#43486=CARTESIAN_POINT('Ctrl Pts',(1.5,3.78100398052407,7.05078912229265));
#43487=CARTESIAN_POINT('Ctrl Pts',(0.,3.90266451604675,6.98418413124666));
#43488=CARTESIAN_POINT('Ctrl Pts',(1.5,3.90266451604675,6.98418413124666));
#43489=CARTESIAN_POINT('Ctrl Pts',(0.,4.02315214109941,6.91548010508983));
#43490=CARTESIAN_POINT('Ctrl Pts',(1.5,4.02315214109941,6.91548010508983));
#43491=CARTESIAN_POINT('Ctrl Pts',(0.,4.14243064422928,6.84469769436163));
#43492=CARTESIAN_POINT('Ctrl Pts',(1.5,4.14243064422928,6.84469769436163));
#43493=CARTESIAN_POINT('Ctrl Pts',(0.,4.26046417733762,6.77185817468256));
#43494=CARTESIAN_POINT('Ctrl Pts',(1.5,4.26046417733762,6.77185817468256));
#43495=CARTESIAN_POINT('Ctrl Pts',(0.,4.37721726637856,6.69698343926911));
#43496=CARTESIAN_POINT('Ctrl Pts',(1.5,4.37721726637856,6.69698343926911));
#43497=CARTESIAN_POINT('Ctrl Pts',(0.,4.4926548220813,6.62009599148732));
#43498=CARTESIAN_POINT('Ctrl Pts',(1.5,4.4926548220813,6.62009599148732));
#43499=CARTESIAN_POINT('Ctrl Pts',(0.,4.60674215069637,6.54121893744448));
#43500=CARTESIAN_POINT('Ctrl Pts',(1.5,4.60674215069637,6.54121893744448));
#43501=CARTESIAN_POINT('Ctrl Pts',(0.,4.71944496476657,6.46037597861856));
#43502=CARTESIAN_POINT('Ctrl Pts',(1.5,4.71944496476657,6.46037597861856));
#43503=CARTESIAN_POINT('Ctrl Pts',(0.,4.83072939299739,6.37759140631321));
#43504=CARTESIAN_POINT('Ctrl Pts',(1.5,4.83072939299739,6.37759140631321));
#43505=CARTESIAN_POINT('Ctrl Pts',(0.,4.9405619901535,6.29289009614967));
#43506=CARTESIAN_POINT('Ctrl Pts',(1.5,4.9405619901535,6.29289009614967));
#43507=CARTESIAN_POINT('Ctrl Pts',(0.,5.04890974698171,6.20629750259518));
#43508=CARTESIAN_POINT('Ctrl Pts',(1.5,5.04890974698171,6.20629750259518));
#43509=CARTESIAN_POINT('Ctrl Pts',(0.,5.15574010016135,6.11783965352734));
#43510=CARTESIAN_POINT('Ctrl Pts',(1.5,5.15574010016135,6.11783965352734));
#43511=CARTESIAN_POINT('Ctrl Pts',(0.,5.26102094228238,6.02754314483433));
#43512=CARTESIAN_POINT('Ctrl Pts',(1.5,5.26102094228238,6.02754314483433));
#43513=CARTESIAN_POINT('Ctrl Pts',(0.,5.36472063146403,5.93543512735866));
#43514=CARTESIAN_POINT('Ctrl Pts',(1.5,5.36472063146403,5.93543512735866));
#43515=CARTESIAN_POINT('Ctrl Pts',(0.,5.46680800100264,5.84154329387568));
#43516=CARTESIAN_POINT('Ctrl Pts',(1.5,5.46680800100264,5.84154329387568));
#43517=CARTESIAN_POINT('Ctrl Pts',(0.,5.56725236904908,5.74589586610586));
#43518=CARTESIAN_POINT('Ctrl Pts',(1.5,5.56725236904908,5.74589586610586));
#43519=CARTESIAN_POINT('Ctrl Pts',(0.,5.66602354831653,5.64852158176032));
#43520=CARTESIAN_POINT('Ctrl Pts',(1.5,5.66602354831653,5.64852158176032));
#43521=CARTESIAN_POINT('Ctrl Pts',(0.,5.76309185581898,5.54944968161887));
#43522=CARTESIAN_POINT('Ctrl Pts',(1.5,5.76309185581898,5.54944968161887));
#43523=CARTESIAN_POINT('Ctrl Pts',(0.,5.85842812070729,5.44870991119888));
#43524=CARTESIAN_POINT('Ctrl Pts',(1.5,5.85842812070729,5.44870991119888));
#43525=CARTESIAN_POINT('Ctrl Pts',(0.,5.95200369213706,5.34633252245584));
#43526=CARTESIAN_POINT('Ctrl Pts',(1.5,5.95200369213706,5.34633252245584));
#43527=CARTESIAN_POINT('Ctrl Pts',(0.,6.04379044716914,5.24234827551538));
#43528=CARTESIAN_POINT('Ctrl Pts',(1.5,6.04379044716914,5.24234827551538));
#43529=CARTESIAN_POINT('Ctrl Pts',(0.,6.13376079870296,5.13678844043658));
#43530=CARTESIAN_POINT('Ctrl Pts',(1.5,6.13376079870296,5.13678844043658));
#43531=CARTESIAN_POINT('Ctrl Pts',(0.,6.22188770344349,5.02968479900663));
#43532=CARTESIAN_POINT('Ctrl Pts',(1.5,6.22188770344349,5.02968479900663));
#43533=CARTESIAN_POINT('Ctrl Pts',(0.,6.30814467128367,4.92106960970541));
#43534=CARTESIAN_POINT('Ctrl Pts',(1.5,6.30814467128367,4.92106960970541));
#43535=CARTESIAN_POINT('Ctrl Pts',(0.,6.39250577472143,4.81097557269961));
#43536=CARTESIAN_POINT('Ctrl Pts',(1.5,6.39250577472143,4.81097557269961));
#43537=CARTESIAN_POINT('Ctrl Pts',(0.,6.47494565831174,4.6994357948647));
#43538=CARTESIAN_POINT('Ctrl Pts',(1.5,6.47494565831174,4.6994357948647));
#43539=CARTESIAN_POINT('Ctrl Pts',(0.,6.55543954815451,4.58648375483325));
#43540=CARTESIAN_POINT('Ctrl Pts',(1.5,6.55543954815451,4.58648375483325));
#43541=CARTESIAN_POINT('Ctrl Pts',(0.,6.63396326141842,4.47215326806801));
#43542=CARTESIAN_POINT('Ctrl Pts',(1.5,6.63396326141842,4.47215326806801));
#43543=CARTESIAN_POINT('Ctrl Pts',(0.,6.71049320933066,4.3564785348024));
#43544=CARTESIAN_POINT('Ctrl Pts',(1.5,6.71049320933066,4.3564785348024));
#43545=CARTESIAN_POINT('Ctrl Pts',(0.,6.7850064002035,4.23949418800588));
#43546=CARTESIAN_POINT('Ctrl Pts',(1.5,6.7850064002035,4.23949418800588));
#43547=CARTESIAN_POINT('Ctrl Pts',(0.,6.85748044249833,4.1212353413755));
#43548=CARTESIAN_POINT('Ctrl Pts',(1.5,6.85748044249833,4.1212353413755));
#43549=CARTESIAN_POINT('Ctrl Pts',(0.,6.92789354792729,4.00173763735536));
#43550=CARTESIAN_POINT('Ctrl Pts',(1.5,6.92789354792729,4.00173763735536));
#43551=CARTESIAN_POINT('Ctrl Pts',(0.,6.99622453459269,3.88103729518557));
#43552=CARTESIAN_POINT('Ctrl Pts',(1.5,6.99622453459269,3.88103729518557));
#43553=CARTESIAN_POINT('Ctrl Pts',(0.,7.06245284183707,3.75917096410964));
#43554=CARTESIAN_POINT('Ctrl Pts',(1.5,7.06245284183707,3.75917096410964));
#43555=CARTESIAN_POINT('Ctrl Pts',(0.,7.12655854513193,3.63617557660714));
#43556=CARTESIAN_POINT('Ctrl Pts',(1.5,7.12655854513193,3.63617557660714));
#43557=CARTESIAN_POINT('Ctrl Pts',(0.,7.18852237100618,3.51208820164565));
#43558=CARTESIAN_POINT('Ctrl Pts',(1.5,7.18852237100618,3.51208820164565));
#43559=CARTESIAN_POINT('Ctrl Pts',(0.,7.24832571201498,3.38694589794629));
#43560=CARTESIAN_POINT('Ctrl Pts',(1.5,7.24832571201498,3.38694589794629));
#43561=CARTESIAN_POINT('Ctrl Pts',(0.,7.30595064174937,3.26078556725682));
#43562=CARTESIAN_POINT('Ctrl Pts',(1.5,7.30595064174937,3.26078556725682));
#43563=CARTESIAN_POINT('Ctrl Pts',(0.,7.36137989899042,3.1336442580578));
#43564=CARTESIAN_POINT('Ctrl Pts',(1.5,7.36137989899042,3.1336442580578));
#43565=CARTESIAN_POINT('Ctrl Pts',(0.,7.41459687190452,3.00555946928163));
#43566=CARTESIAN_POINT('Ctrl Pts',(1.5,7.41459687190452,3.00555946928163));
#43567=CARTESIAN_POINT('Ctrl Pts',(0.,7.4655855822794,2.87656945405601));
#43568=CARTESIAN_POINT('Ctrl Pts',(1.5,7.4655855822794,2.87656945405601));
#43569=CARTESIAN_POINT('Ctrl Pts',(0.,7.51433066980066,2.74671352348252));
#43570=CARTESIAN_POINT('Ctrl Pts',(1.5,7.51433066980066,2.74671352348252));
#43571=CARTESIAN_POINT('Ctrl Pts',(0.,7.56081737636802,2.61603235046252));
#43572=CARTESIAN_POINT('Ctrl Pts',(1.5,7.56081737636802,2.61603235046252));
#43573=CARTESIAN_POINT('Ctrl Pts',(0.,7.60503159823037,2.48456722613382));
#43574=CARTESIAN_POINT('Ctrl Pts',(1.5,7.60503159823037,2.48456722613382));
#43575=CARTESIAN_POINT('Ctrl Pts',(0.,7.64695993816224,2.35235931633758));
#43576=CARTESIAN_POINT('Ctrl Pts',(1.5,7.64695993816224,2.35235931633758));
#43577=CARTESIAN_POINT('Ctrl Pts',(0.,7.68658975768392,2.21944891808583));
#43578=CARTESIAN_POINT('Ctrl Pts',(1.5,7.68658975768392,2.21944891808583));
#43579=CARTESIAN_POINT('Ctrl Pts',(0.,7.72390922932699,2.0858747160024));
#43580=CARTESIAN_POINT('Ctrl Pts',(1.5,7.72390922932699,2.0858747160024));
#43581=CARTESIAN_POINT('Ctrl Pts',(0.,7.7589073889478,1.95167303870691));
#43582=CARTESIAN_POINT('Ctrl Pts',(1.5,7.7589073889478,1.95167303870691));
#43583=CARTESIAN_POINT('Ctrl Pts',(0.,7.79157402704055,1.81687953471803));
#43584=CARTESIAN_POINT('Ctrl Pts',(1.5,7.79157402704055,1.81687953471803));
#43585=CARTESIAN_POINT('Ctrl Pts',(0.,7.8218995800964,1.68153084833423));
#43586=CARTESIAN_POINT('Ctrl Pts',(1.5,7.8218995800964,1.68153084833423));
#43587=CARTESIAN_POINT('Ctrl Pts',(0.,7.84987502200416,1.54566629555745));
#43588=CARTESIAN_POINT('Ctrl Pts',(1.5,7.84987502200416,1.54566629555745));
#43589=CARTESIAN_POINT('Ctrl Pts',(0.,7.87549175548865,1.40932954012019));
#43590=CARTESIAN_POINT('Ctrl Pts',(1.5,7.87549175548865,1.40932954012019));
#43591=CARTESIAN_POINT('Ctrl Pts',(0.,7.89874150358258,1.27257026968328));
#43592=CARTESIAN_POINT('Ctrl Pts',(1.5,7.89874150358258,1.27257026968328));
#43593=CARTESIAN_POINT('Ctrl Pts',(0.,7.91961655999428,1.13544052228966));
#43594=CARTESIAN_POINT('Ctrl Pts',(1.5,7.91961655999428,1.13544052228966));
#43595=CARTESIAN_POINT('Ctrl Pts',(0.,7.93811003951429,0.99799101291279));
#43596=CARTESIAN_POINT('Ctrl Pts',(1.5,7.93811003951429,0.99799101291279));
#43597=CARTESIAN_POINT('Ctrl Pts',(0.,7.95421612847067,0.860267459956574));
#43598=CARTESIAN_POINT('Ctrl Pts',(1.5,7.95421612847067,0.860267459956574));
#43599=CARTESIAN_POINT('Ctrl Pts',(0.,7.96793033524234,0.722306911570933));
#43600=CARTESIAN_POINT('Ctrl Pts',(1.5,7.96793033524234,0.722306911570933));
#43601=CARTESIAN_POINT('Ctrl Pts',(0.,7.97924974084015,0.584134071639387));
#43602=CARTESIAN_POINT('Ctrl Pts',(1.5,7.97924974084015,0.584134071639387));
#43603=CARTESIAN_POINT('Ctrl Pts',(0.,7.988172666211,0.445763767776282));
#43604=CARTESIAN_POINT('Ctrl Pts',(1.5,7.988172666211,0.445763767776282));
#43605=CARTESIAN_POINT('Ctrl Pts',(0.,7.99339320492744,0.334915488715433));
#43606=CARTESIAN_POINT('Ctrl Pts',(1.5,7.99339320492744,0.334915488715433));
#43607=CARTESIAN_POINT('Ctrl Pts',(0.,7.9962297569157,0.251694874137988));
#43608=CARTESIAN_POINT('Ctrl Pts',(1.5,7.9962297569157,0.251694874137988));
#43609=CARTESIAN_POINT('Ctrl Pts',(0.,7.99764130779673,0.196176951432127));
#43610=CARTESIAN_POINT('Ctrl Pts',(1.5,7.99764130779673,0.196176951432127));
#43611=CARTESIAN_POINT('Ctrl Pts',(0.,7.99822721229278,0.168408611832292));
#43612=CARTESIAN_POINT('Ctrl Pts',(1.5,7.99822721229278,0.168408611832292));
#43613=CARTESIAN_POINT('',(0.15,7.99822721229278,0.168408611832292));
#43614=CARTESIAN_POINT('Ctrl Pts',(0.15,7.99822721229278,0.168408611832292));
#43615=CARTESIAN_POINT('Ctrl Pts',(0.15,7.9668162212544,1.6571001514885));
#43616=CARTESIAN_POINT('Ctrl Pts',(0.15,7.05454066693418,4.60748407596604));
#43617=CARTESIAN_POINT('Ctrl Pts',(0.15,3.54676252795573,7.6458195669611));
#43618=CARTESIAN_POINT('Ctrl Pts',(0.15,-1.03566271747928,8.36163178448781));
#43619=CARTESIAN_POINT('Ctrl Pts',(0.15,-5.30396918600683,6.54797121169431));
#43620=CARTESIAN_POINT('Ctrl Pts',(0.15,-7.96648062384354,2.74828140568407));
#43621=CARTESIAN_POINT('Ctrl Pts',(0.15,-8.19387712094983,-1.54631831555544));
#43622=CARTESIAN_POINT('Ctrl Pts',(0.15,-6.51467119594908,-5.07412386813192));
#43623=CARTESIAN_POINT('Ctrl Pts',(0.15,-3.76134237152816,-7.35225187872476));
#43624=CARTESIAN_POINT('Ctrl Pts',(0.15,-0.301346652009213,-8.25272087673402));
#43625=CARTESIAN_POINT('Ctrl Pts',(0.15,3.21364811100624,-7.60713764510347));
#43626=CARTESIAN_POINT('Ctrl Pts',(0.15,6.12799056084021,-5.53596483741694));
#43627=CARTESIAN_POINT('Ctrl Pts',(0.15,7.42100104272284,-3.25862403370716));
#43628=CARTESIAN_POINT('Ctrl Pts',(0.15,7.90104362420642,-1.41473238843176));
#43629=CARTESIAN_POINT('Ctrl Pts',(0.15,7.98748469629358,-0.677499195126446));
#43630=CARTESIAN_POINT('Ctrl Pts',(0.15,7.99822707315249,-0.168415205726119));
#43631=CARTESIAN_POINT('',(0.,7.99822721229278,0.168408611832292));
#43632=CARTESIAN_POINT('Ctrl Pts',(0.15,7.99822735142219,-0.168402017937099));
#43633=CARTESIAN_POINT('Ctrl Pts',(0.15,7.98748572261181,-0.677490441897062));
#43634=CARTESIAN_POINT('Ctrl Pts',(0.15,7.90104473181587,-1.41472813399292));
#43635=CARTESIAN_POINT('Ctrl Pts',(0.15,7.42100104272284,-3.25862403370716));
#43636=CARTESIAN_POINT('Ctrl Pts',(0.15,6.12799056084021,-5.53596483741694));
#43637=CARTESIAN_POINT('Ctrl Pts',(0.15,3.21364811100624,-7.60713764510347));
#43638=CARTESIAN_POINT('Ctrl Pts',(0.15,-0.301346652009213,-8.25272087673402));
#43639=CARTESIAN_POINT('Ctrl Pts',(0.15,-3.76134237152816,-7.35225187872476));
#43640=CARTESIAN_POINT('Ctrl Pts',(0.15,-6.51467119594908,-5.07412386813192));
#43641=CARTESIAN_POINT('Ctrl Pts',(0.15,-8.19387712094983,-1.54631831555544));
#43642=CARTESIAN_POINT('Ctrl Pts',(0.15,-7.96648062384354,2.74828140568407));
#43643=CARTESIAN_POINT('Ctrl Pts',(0.15,-5.30396918600683,6.54797121169431));
#43644=CARTESIAN_POINT('Ctrl Pts',(0.15,-1.03566271747928,8.36163178448781));
#43645=CARTESIAN_POINT('Ctrl Pts',(0.15,3.54676252795573,7.6458195669611));
#43646=CARTESIAN_POINT('Ctrl Pts',(0.15,7.05454066693418,4.60748407596604));
#43647=CARTESIAN_POINT('Ctrl Pts',(0.15,7.9668162212544,1.6571001514885));
#43648=CARTESIAN_POINT('Ctrl Pts',(0.15,7.99822721229278,0.168408611832292));
#43649=CARTESIAN_POINT('Ctrl Pts',(0.1,8.04821622517087,-0.169456769727133));
#43650=CARTESIAN_POINT('Ctrl Pts',(0.1,8.03741002472644,-0.681720507360159));
#43651=CARTESIAN_POINT('Ctrl Pts',(0.1,7.95042407944463,-1.42356971720002));
#43652=CARTESIAN_POINT('Ctrl Pts',(0.1,7.46738625004804,-3.2789905004189));
#43653=CARTESIAN_POINT('Ctrl Pts',(0.1,6.16628997740278,-5.57056470636502));
#43654=CARTESIAN_POINT('Ctrl Pts',(0.1,3.23373517685434,-7.65468305150081));
#43655=CARTESIAN_POINT('Ctrl Pts',(0.1,-0.303229672299122,-8.30429995047224));
#43656=CARTESIAN_POINT('Ctrl Pts',(0.1,-3.7848514261649,-7.39820381482444));
#43657=CARTESIAN_POINT('Ctrl Pts',(0.1,-6.55538636377591,-5.10583648537583));
#43658=CARTESIAN_POINT('Ctrl Pts',(0.1,-8.24508930199638,-1.55598312295372));
#43659=CARTESIAN_POINT('Ctrl Pts',(0.1,-8.01627176717492,2.76545880984833));
#43660=CARTESIAN_POINT('Ctrl Pts',(0.1,-5.33711785417695,6.58889573792462));
#43661=CARTESIAN_POINT('Ctrl Pts',(0.1,-1.04213746891484,8.41389837754811));
#43662=CARTESIAN_POINT('Ctrl Pts',(0.1,3.56893478939425,7.69359494724594));
#43663=CARTESIAN_POINT('Ctrl Pts',(0.1,7.09862217307051,4.63628718819819));
#43664=CARTESIAN_POINT('Ctrl Pts',(0.1,8.01662992354949,1.6674436985376));
#43665=CARTESIAN_POINT('Ctrl Pts',(0.1,8.04821608604147,0.169463363621706));
#43666=CARTESIAN_POINT('Ctrl Pts',(0.05,8.09820509891955,-0.170511521517167));
#43667=CARTESIAN_POINT('Ctrl Pts',(0.0499999999999999,8.08752804174321,
-0.676424631804066));
#43668=CARTESIAN_POINT('Ctrl Pts',(0.05,7.99982927879915,-1.43151013980792));
#43669=CARTESIAN_POINT('Ctrl Pts',(0.0499999999999999,7.51385392106967,
-3.2948434841773));
#43670=CARTESIAN_POINT('Ctrl Pts',(0.0500000000000001,6.20457757618847,
-5.60581111430041));
#43671=CARTESIAN_POINT('Ctrl Pts',(0.0499999999999999,3.25384581479248,
-7.70084002943972));
#43672=CARTESIAN_POINT('Ctrl Pts',(0.05,-0.305119682800658,-8.35615970982999));
#43673=CARTESIAN_POINT('Ctrl Pts',(0.05,-3.80835338172119,-7.44390937025256));
#43674=CARTESIAN_POINT('Ctrl Pts',(0.05,-6.59610752261337,-5.13761912738161));
#43675=CARTESIAN_POINT('Ctrl Pts',(0.05,-8.29629911008737,-1.56559713102122));
#43676=CARTESIAN_POINT('Ctrl Pts',(0.05,-8.06606138615749,2.78261373021506));
#43677=CARTESIAN_POINT('Ctrl Pts',(0.05,-5.37026983572066,6.62982849821033));
#43678=CARTESIAN_POINT('Ctrl Pts',(0.05,-1.04860644953161,8.46614583459751));
#43679=CARTESIAN_POINT('Ctrl Pts',(0.0499999999999999,3.59109175735748,
7.741390063858));
#43680=CARTESIAN_POINT('Ctrl Pts',(0.0500000000000001,7.14273392056364,
4.66508468971586));
#43681=CARTESIAN_POINT('Ctrl Pts',(0.0499999999999999,8.06638259247629,
1.67771968477482));
#43682=CARTESIAN_POINT('Ctrl Pts',(0.05,8.09820495979016,0.170518115411121));
#43683=CARTESIAN_POINT('Ctrl Pts',(0.,8.14819397266823,-0.171566273307201));
#43684=CARTESIAN_POINT('Ctrl Pts',(0.,8.13745234385785,-0.680654697267163));
#43685=CARTESIAN_POINT('Ctrl Pts',(0.,8.04920862642792,-1.44035172301502));
#43686=CARTESIAN_POINT('Ctrl Pts',(0.,7.56023912839487,-3.31520995088904));
#43687=CARTESIAN_POINT('Ctrl Pts',(0.,6.24287699275104,-5.64041098324849));
#43688=CARTESIAN_POINT('Ctrl Pts',(0.,3.27393288064058,-7.74838543583707));
#43689=CARTESIAN_POINT('Ctrl Pts',(0.,-0.307002703090567,-8.40773878356821));
#43690=CARTESIAN_POINT('Ctrl Pts',(0.,-3.83186243635793,-7.48986130635224));
#43691=CARTESIAN_POINT('Ctrl Pts',(0.,-6.6368226904402,-5.16933174462552));
#43692=CARTESIAN_POINT('Ctrl Pts',(0.,-8.34751129113392,-1.5752619384195));
#43693=CARTESIAN_POINT('Ctrl Pts',(0.,-8.11585252948887,2.79979113437932));
#43694=CARTESIAN_POINT('Ctrl Pts',(0.,-5.40341850389078,6.67075302444065));
#43695=CARTESIAN_POINT('Ctrl Pts',(0.,-1.05508120096718,8.51841242765781));
#43696=CARTESIAN_POINT('Ctrl Pts',(0.,3.61326401879599,7.78916544414284));
#43697=CARTESIAN_POINT('Ctrl Pts',(0.,7.18681542669997,4.693887801948));
#43698=CARTESIAN_POINT('Ctrl Pts',(0.,8.11619629477138,1.68806323182392));
#43699=CARTESIAN_POINT('Ctrl Pts',(0.,8.14819383353886,0.171572867200535));
#43700=CARTESIAN_POINT('',(0.,8.14819390295858,0.171569570250815));
#43701=CARTESIAN_POINT('Ctrl Pts',(0.,8.14819383353886,0.171572867200535));
#43702=CARTESIAN_POINT('Ctrl Pts',(0.05,8.09820495979016,0.170518115411121));
#43703=CARTESIAN_POINT('Ctrl Pts',(0.1,8.04821608604147,0.169463363621706));
#43704=CARTESIAN_POINT('Ctrl Pts',(0.15,7.99822721229278,0.168408611832292));
#43705=CARTESIAN_POINT('Ctrl Pts',(0.,8.14819397266823,-0.171566273307201));
#43706=CARTESIAN_POINT('Ctrl Pts',(0.,8.13745234385785,-0.680654697267163));
#43707=CARTESIAN_POINT('Ctrl Pts',(0.,8.04920862642792,-1.44035172301502));
#43708=CARTESIAN_POINT('Ctrl Pts',(0.,7.56023912839487,-3.31520995088904));
#43709=CARTESIAN_POINT('Ctrl Pts',(0.,6.24287699275104,-5.64041098324849));
#43710=CARTESIAN_POINT('Ctrl Pts',(0.,3.27393288064058,-7.74838543583707));
#43711=CARTESIAN_POINT('Ctrl Pts',(0.,-0.307002703090567,-8.40773878356821));
#43712=CARTESIAN_POINT('Ctrl Pts',(0.,-3.83186243635793,-7.48986130635224));
#43713=CARTESIAN_POINT('Ctrl Pts',(0.,-6.6368226904402,-5.16933174462552));
#43714=CARTESIAN_POINT('Ctrl Pts',(0.,-8.34751129113392,-1.5752619384195));
#43715=CARTESIAN_POINT('Ctrl Pts',(0.,-8.11585252948887,2.79979113437932));
#43716=CARTESIAN_POINT('Ctrl Pts',(0.,-5.40341850389078,6.67075302444065));
#43717=CARTESIAN_POINT('Ctrl Pts',(0.,-1.05508120096718,8.51841242765781));
#43718=CARTESIAN_POINT('Ctrl Pts',(0.,3.61326401879599,7.78916544414284));
#43719=CARTESIAN_POINT('Ctrl Pts',(0.,7.18681542669997,4.693887801948));
#43720=CARTESIAN_POINT('Ctrl Pts',(0.,8.11619629477138,1.68806323182392));
#43721=CARTESIAN_POINT('Ctrl Pts',(0.,8.14819383353886,0.171572867200535));
#43722=CARTESIAN_POINT('Origin',(0.,7.99822721229278,0.168408611832292));
#43723=CARTESIAN_POINT('',(1.5,7.99822721229278,0.168408611832292));
#43724=CARTESIAN_POINT('',(0.,7.99822721229278,0.168408611832292));
#43725=CARTESIAN_POINT('Origin',(1.5,-0.00140950834140008,9.76996261670138E-14));
#43726=CARTESIAN_POINT('Origin',(0.,-0.00140950834140008,9.76996261670138E-14));
#60344=UNCERTAINTY_MEASURE_WITH_UNIT(LENGTH_MEASURE(0.01),#60366,
'DISTANCE_ACCURACY_VALUE',
'Maximum model space distance between geometric entities at asserted c
onnectivities');
#60353=UNCERTAINTY_MEASURE_WITH_UNIT(LENGTH_MEASURE(0.01),#60366,
'DISTANCE_ACCURACY_VALUE',
'Maximum model space distance between geometric entities at asserted c
onnectivities');
#60356=(
GEOMETRIC_REPRESENTATION_CONTEXT(3)
GLOBAL_UNCERTAINTY_ASSIGNED_CONTEXT((#60344))
GLOBAL_UNIT_ASSIGNED_CONTEXT((#60366,#60368,#60369))
REPRESENTATION_CONTEXT('','3D')
);
#60365=(
GEOMETRIC_REPRESENTATION_CONTEXT(3)
GLOBAL_UNCERTAINTY_ASSIGNED_CONTEXT((#60353))
GLOBAL_UNIT_ASSIGNED_CONTEXT((#60366,#60368,#60369))
REPRESENTATION_CONTEXT('','3D')
);
#60366=(
LENGTH_UNIT()
NAMED_UNIT(*)
SI_UNIT(.MILLI.,.METRE.)
);
#60368=(
NAMED_UNIT(*)
PLANE_ANGLE_UNIT()
SI_UNIT($,.RADIAN.)
);
#60369=(
NAMED_UNIT(*)
SI_UNIT($,.STERADIAN.)
SOLID_ANGLE_UNIT()
);
#60372=SHAPE_DEFINITION_REPRESENTATION(#60383,#60408);
#60383=PRODUCT_DEFINITION_SHAPE('',$,#60420);
#60408=SHAPE_REPRESENTATION('',(#18916),#60356);
#60417=PRODUCT_DEFINITION_CONTEXT('part definition',#60452,'design');
#60420=PRODUCT_DEFINITION('2026-10-25-00-06-27-341',
'02_Piston_Ring_Turbine_D19',#60431,#60417);
#60431=PRODUCT_DEFINITION_FORMATION('',$,#60456);
#60452=APPLICATION_CONTEXT(
'Core Data for Automotive Mechanical Design Process');
#60453=PRODUCT_CONTEXT('part definition',#60452,'mechanical');
#60456=PRODUCT('2026-10-25-00-06-27-341','02_Piston_Ring_Turbine_D19',$,
(#60453));
#60514=COLOUR_RGB('Sky Blue',0.24,0.69,0.87);
#60515=FILL_AREA_STYLE_COLOUR('',#60514);
#60516=FILL_AREA_STYLE('',(#60515));
#60517=SURFACE_STYLE_FILL_AREA(#60516);
#60518=SURFACE_SIDE_STYLE('',(#60517));
#60519=SURFACE_STYLE_USAGE(.BOTH.,#60518);
#60520=PRESENTATION_STYLE_ASSIGNMENT((#60519));
ENDSEC;
END-ISO-10303-21;
